ISO-10303-21;
HEADER;
FILE_DESCRIPTION (('STEP AP214'),
    '1' );
FILE_NAME ('hexagon nut style 1_is_IS 1364-3 - M16-W-N.step',
    '2026-10-26T19:46:16',
    ( '' ),
    ( '' ),
    'SwSTEP 2.0',
    'SolidWorks 2025',
    '' );
FILE_SCHEMA (( 'AUTOMOTIVE_DESIGN' ));
ENDSEC;

DATA;
#19=VERTEX_POINT ( 'NONE', #73420 ) ;
#58=CARTESIAN_POINT ( 'NONE',  ( 12.00000000000000178, -4.647306338817273286, -0.4736860157878156619 ) ) ;
#75=EDGE_LOOP ( 'NONE', ( #23247, #62636, #23741 ) ) ;
#122=EDGE_LOOP ( 'NONE', ( #35073, #51251, #40742, #51400, #60040, #5045 ) ) ;
#139=FACE_OUTER_BOUND ( 'NONE', #14459, .T. ) ;
#458=DIRECTION ( 'NONE',  ( 0.000000000000000000, 0.000000000000000000, -1.000000000000000000 ) ) ;
#729=CARTESIAN_POINT ( 'NONE',  ( 6.000000000000023093, 10.39230484541324984, 0.000000000000000000 ) ) ;
#761=EDGE_LOOP ( 'NONE', ( #29482, #20834, #25330, #23440, #49814, #57819 ) ) ;
#876=PLANE ( 'NONE',  #50648 ) ;
#883=VECTOR ( 'NONE', #74149, 1000.000000000000000 ) ;
#919=DIRECTION ( 'NONE',  ( 1.000000000000000000, 0.000000000000000000, 0.000000000000000000 ) ) ;
#1122=CARTESIAN_POINT ( 'NONE',  ( 8.000000000000003553, 0.000000000000000000, -14.80000000000000071 ) ) ;
#1173=CARTESIAN_POINT ( 'NONE',  ( 4.979315568031101868, -10.98159727696820731, -0.02533325329317183752 ) ) ;
#1288=DIRECTION ( 'NONE',  ( -0.000000000000000000, -0.000000000000000000, 1.000000000000000000 ) ) ;
#1319=EDGE_CURVE ( 'NONE', #39861, #70940, #23217, .T. ) ;
#1358=VECTOR ( 'NONE', #57601, 1000.000000000000000 ) ;
#1410=EDGE_CURVE ( 'NONE', #3350, #5379, #66560, .T. ) ;
#1491=CARTESIAN_POINT ( 'NONE',  ( 0.000000000000000000, 0.000000000000000000, 0.000000000000000000 ) ) ;
#1569=CARTESIAN_POINT ( 'NONE',  ( -12.00000000000000000, 6.928203230275504332, -14.00000000000000178 ) ) ;
#1582=EDGE_LOOP ( 'NONE', ( #37871, #41850, #68765, #14821, #16320, #25666 ) ) ;
#1649=ORIENTED_EDGE ( 'NONE', *, *, #19501, .T. ) ;
#1762=CARTESIAN_POINT ( 'NONE',  ( 12.00000000000000000, 6.928203230275542523, -1.071796769724504550 ) ) ;
#1895=CARTESIAN_POINT ( 'NONE',  ( 6.000000000000011546, -10.39230484541325694, 0.000000000000000000 ) ) ;
#1987=ADVANCED_FACE ( 'NONE', ( #65917 ), #70843, .T. ) ;
#1996=EDGE_CURVE ( 'NONE', #58040, #48595, #31598, .T. ) ;
#2055=CARTESIAN_POINT ( 'NONE',  ( -12.00000000000000000, 0.000000000000000000, -14.00000000000000178 ) ) ;
#2206=DIRECTION ( 'NONE',  ( -1.000000000000000000, 0.000000000000000000, 0.000000000000000000 ) ) ;
#2244=CIRCLE ( 'NONE', #57695, 8.000000000000003553 ) ;
#2263=CARTESIAN_POINT ( 'NONE',  ( 12.00000000000000000, 6.928203230275491009, -14.80000000000000071 ) ) ;
#2281=DIRECTION ( 'NONE',  ( 0.000000000000000000, -0.000000000000000000, 1.000000000000000000 ) ) ;
#2293=AXIS2_PLACEMENT_3D ( 'NONE', #6357, #29361, #22559 ) ;
#2308=CARTESIAN_POINT ( 'NONE',  ( -8.032507269244980819, -9.218836226384828691, -0.1233701403699506427 ) ) ;
#2353=EDGE_LOOP ( 'NONE', ( #21587, #66906, #37007, #17066 ) ) ;
#2418=CARTESIAN_POINT ( 'NONE',  ( 12.00000000000000355, 0.000000000000000000, -14.80000000000000071 ) ) ;
#2799=DIRECTION ( 'NONE',  ( -1.000000000000000000, 0.000000000000000000, 0.000000000000000000 ) ) ;
#2835=ORIENTED_EDGE ( 'NONE', *, *, #7521, .T. ) ;
#2926=VECTOR ( 'NONE', #52722, 1000.000000000000000 ) ;
#2954=EDGE_CURVE ( 'NONE', #6656, #42139, #37669, .T. ) ;
#3055=AXIS2_PLACEMENT_3D ( 'NONE', #56877, #5561, #4821 ) ;
#3141=DIRECTION ( 'NONE',  ( 1.000000000000000000, 0.000000000000000000, 0.000000000000000000 ) ) ;
#3231=ORIENTED_EDGE ( 'NONE', *, *, #27662, .F. ) ;
#3326=VECTOR ( 'NONE', #41230, 1000.000000000000114 ) ;
#3350=VERTEX_POINT ( 'NONE', #16108 ) ;
#3473=DIRECTION ( 'NONE',  ( 1.000000000000000000, 0.000000000000000000, 0.000000000000000000 ) ) ;
#3603=EDGE_LOOP ( 'NONE', ( #25086, #65949, #20405, #65687, #67874, #65968 ) ) ;
#3675=ORIENTED_EDGE ( 'NONE', *, *, #42128, .T. ) ;
#3880=EDGE_CURVE ( 'NONE', #39861, #29704, #65492, .T. ) ;
#3950=CARTESIAN_POINT ( 'NONE',  ( 0.000000000000000000, 0.000000000000000000, 0.000000000000000000 ) ) ;
#3951=EDGE_CURVE ( 'NONE', #22045, #37361, #31343, .T. ) ;
#3979=CARTESIAN_POINT ( 'NONE',  ( 10.02978802437157135, -8.065705644765241544, -0.4750804646944294385 ) ) ;
#4053=EDGE_LOOP ( 'NONE', ( #42676, #3231, #49429 ) ) ;
#4134=PLANE ( 'NONE',  #44373 ) ;
#4293=ADVANCED_FACE ( 'NONE', ( #20688 ), #72761, .F. ) ;
#4625=EDGE_CURVE ( 'NONE', #12103, #47682, #44691, .T. ) ;
#4638=EDGE_CURVE ( 'NONE', #15222, #39861, #24772, .T. ) ;
#4821=DIRECTION ( 'NONE',  ( 1.000000000000000000, 0.000000000000000000, 0.000000000000000000 ) ) ;
#4861=CARTESIAN_POINT ( 'NONE',  ( 0.000000000000000000, 0.000000000000000000, 0.000000000000000000 ) ) ;
#5045=ORIENTED_EDGE ( 'NONE', *, *, #20935, .F. ) ;
#5167=ORIENTED_EDGE ( 'NONE', *, *, #74467, .F. ) ;
#5257=CARTESIAN_POINT ( 'NONE',  ( 6.509199954993393433, 10.09831811432648685, 6.904800827780242789E-15 ) ) ;
#5281=CARTESIAN_POINT ( 'NONE',  ( 0.000000000000000000, 23.85640646055104241, -14.00000000000000178 ) ) ;
#5361=EDGE_CURVE ( 'NONE', #26153, #68525, #32605, .T. ) ;
#5379=VERTEX_POINT ( 'NONE', #45298 ) ;
#5523=DIRECTION ( 'NONE',  ( -0.8191520442889907994, 0.000000000000000000, -0.5735764363510476027 ) ) ;
#5561=DIRECTION ( 'NONE',  ( -0.000000000000000000, -0.000000000000000000, 1.000000000000000000 ) ) ;
#5653=CARTESIAN_POINT ( 'NONE',  ( 8.000000000000005329, 9.797174393178833546E-16, -14.77459999999999951 ) ) ;
#5661=ORIENTED_EDGE ( 'NONE', *, *, #3951, .T. ) ;
#5698=CARTESIAN_POINT ( 'NONE',  ( 12.00000000000000355, -6.928203230275539859, -1.071796769724504550 ) ) ;
#5823=ADVANCED_FACE ( 'NONE', ( #48539 ), #42877, .F. ) ;
#6304=EDGE_CURVE ( 'NONE', #29704, #56610, #46978, .T. ) ;
#6333=VECTOR ( 'NONE', #36829, 1000.000000000000000 ) ;
#6357=CARTESIAN_POINT ( 'NONE',  ( 12.00000000000000000, 6.928203230275491009, -14.80000000000000071 ) ) ;
#6413=EDGE_CURVE ( 'NONE', #70940, #64507, #54133, .T. ) ;
#6454=CARTESIAN_POINT ( 'NONE',  ( 0.000000000000000000, 0.000000000000000000, 0.000000000000000000 ) ) ;
#6543=ORIENTED_EDGE ( 'NONE', *, *, #48064, .T. ) ;
#6656=VERTEX_POINT ( 'NONE', #50689 ) ;
#6772=CARTESIAN_POINT ( 'NONE',  ( 0.000000000000000000, 0.000000000000000000, -14.80000000000000071 ) ) ;
#6828=CARTESIAN_POINT ( 'NONE',  ( 11.99999999999999822, 0.5857239961182074683, -4.955142741437655135E-17 ) ) ;
#6960=ORIENTED_EDGE ( 'NONE', *, *, #71294, .T. ) ;
#7081=ORIENTED_EDGE ( 'NONE', *, *, #41593, .T. ) ;
#7139=EDGE_CURVE ( 'NONE', #26153, #37361, #41607, .T. ) ;
#7247=CIRCLE ( 'NONE', #49407, 12.00000000000000000 ) ;
#7290=AXIS2_PLACEMENT_3D ( 'NONE', #14843, #49180, #2799 ) ;
#7388=VECTOR ( 'NONE', #66182, 1000.000000000000000 ) ;
#7393=CARTESIAN_POINT ( 'NONE',  ( 11.99999999999999822, -6.928203230275538971, -14.00000000000000178 ) ) ;
#7521=EDGE_CURVE ( 'NONE', #72263, #12103, #21793, .T. ) ;
#7597=ORIENTED_EDGE ( 'NONE', *, *, #67828, .T. ) ;
#7811=CARTESIAN_POINT ( 'NONE',  ( -6.000000000000012434, 10.39230484541325694, 0.000000000000000000 ) ) ;
#8076=ORIENTED_EDGE ( 'NONE', *, *, #15788, .F. ) ;
#8256=AXIS2_PLACEMENT_3D ( 'NONE', #3950, #72213, #60528 ) ;
#8293=DIRECTION ( 'NONE',  ( 1.000000000000000000, 0.000000000000000000, 0.000000000000000000 ) ) ;
#8307=ORIENTED_EDGE ( 'NONE', *, *, #9063, .T. ) ;
#8493=CONICAL_SURFACE ( 'NONE', #55478, 6.900000000000001243, 0.9599310885968755924 ) ;
#8714=CARTESIAN_POINT ( 'NONE',  ( -8.535034553343571417, -8.928701963635374383, -0.1959795092987848819 ) ) ;
#8898=ORIENTED_EDGE ( 'NONE', *, *, #35227, .F. ) ;
#9055=DIRECTION ( 'NONE',  ( 0.000000000000000000, -1.000000000000000000, 0.000000000000000000 ) ) ;
#9063=EDGE_CURVE ( 'NONE', #52340, #21543, #21469, .T. ) ;
#9133=ORIENTED_EDGE ( 'NONE', *, *, #56617, .F. ) ;
#9209=CARTESIAN_POINT ( 'NONE',  ( -12.00000000000000000, 6.928203230275504332, -14.80000000000000071 ) ) ;
#9423=DIRECTION ( 'NONE',  ( 0.000000000000000000, -0.000000000000000000, 1.000000000000000000 ) ) ;
#9573=CONICAL_SURFACE ( 'NONE', #32472, 12.00000000000000000, 1.047197551196596077 ) ;
#9579=EDGE_LOOP ( 'NONE', ( #63358, #10502, #8307, #59673, #42515, #59466 ) ) ;
#9589=CARTESIAN_POINT ( 'NONE',  ( -12.00000000000000000, -6.928203230275542523, -1.071796769724504550 ) ) ;
#9593=FACE_OUTER_BOUND ( 'NONE', #9579, .T. ) ;
#10127=DIRECTION ( 'NONE',  ( 1.000000000000000000, 0.000000000000000000, 0.000000000000000000 ) ) ;
#10147=EDGE_CURVE ( 'NONE', #58040, #47682, #57505, .T. ) ;
#10217=AXIS2_PLACEMENT_3D ( 'NONE', #66847, #15521, #3473 ) ;
#10489=ORIENTED_EDGE ( 'NONE', *, *, #1410, .T. ) ;
#10502=ORIENTED_EDGE ( 'NONE', *, *, #19686, .T. ) ;
#10549=CLOSED_SHELL ( 'NONE', ( #4293, #44739, #22738, #13893, #24172, #13786, #22942, #53767, #54158, #73543, #52607, #46390, #43184, #58468, #61337, #62622, #45549, #1987, #74407, #53589, #11294, #29844, #37509, #55152, #60621, #37771, #26007, #30832, #44347, #5823 ) ) ;
#11025=AXIS2_PLACEMENT_3D ( 'NONE', #73555, #20749, #66779 ) ;
#11069=VECTOR ( 'NONE', #45509, 1000.000000000000114 ) ;
#11085=( LENGTH_UNIT ( ) NAMED_UNIT ( * ) SI_UNIT ( .MILLI., .METRE. ) );
#11098=EDGE_CURVE ( 'NONE', #62698, #72148, #74235, .T. ) ;
#11196=EDGE_LOOP ( 'NONE', ( #45935, #23638, #51313 ) ) ;
#11282=CARTESIAN_POINT ( 'NONE',  ( 8.032507269244971937, 9.218836226384805599, -0.1233701403699331844 ) ) ;
#11294=ADVANCED_FACE ( 'NONE', ( #58031 ), #64412, .T. ) ;
#11422=DIRECTION ( 'NONE',  ( 0.000000000000000000, 0.000000000000000000, 1.000000000000000000 ) ) ;
#11437=EDGE_CURVE ( 'NONE', #64507, #57691, #47415, .T. ) ;
#11571=CIRCLE ( 'NONE', #56157, 8.000000000000000000 ) ;
#11618=EDGE_LOOP ( 'NONE', ( #32871, #27831, #23424 ) ) ;
#11732=CARTESIAN_POINT ( 'NONE',  ( 3.464965446656449899, -11.85590772719120878, -0.1959795092987934584 ) ) ;
#11999=PLANE ( 'NONE',  #2293 ) ;
#12028=DIRECTION ( 'NONE',  ( 0.000000000000000000, 0.000000000000000000, -1.000000000000000000 ) ) ;
#12103=VERTEX_POINT ( 'NONE', #53000 ) ;
#12104=CIRCLE ( 'NONE', #45823, 7.000000000000000000 ) ;
#12307=ORIENTED_EDGE ( 'NONE', *, *, #30530, .T. ) ;
#12441=PRODUCT_DEFINITION_CONTEXT ( 'detailed design', #50548, 'design' ) ;
#12506=ORIENTED_EDGE ( 'NONE', *, *, #2954, .T. ) ;
#12529=ORIENTED_EDGE ( 'NONE', *, *, #34553, .F. ) ;
#12799=SHAPE_REPRESENTATION_RELATIONSHIP ( 'NONE' , 'NONE' ,  #69137, #72247 ) ;
#12828=CARTESIAN_POINT ( 'NONE',  ( 0.9790701977573584847, -13.29114001832031633, -0.7454400371385776491 ) ) ;
#12862=B_SPLINE_CURVE_WITH_KNOTS ( 'NONE', 3,
 ( #15638, #66963, #3979, #43954, #21307, #72999 ),
 .UNSPECIFIED., .F., .F.,
 ( 4, 2, 4 ),
 ( 2.380729645499014578E-07, 0.003505341553885837295, 0.007010445034807124762 ),
 .UNSPECIFIED. ) ;
#12918=DIRECTION ( 'NONE',  ( -0.000000000000000000, -0.000000000000000000, 1.000000000000000000 ) ) ;
#13192=CARTESIAN_POINT ( 'NONE',  ( 3.967492730755045383, -11.56577346444175269, -0.1233701403699556803 ) ) ;
#13215=ORIENTED_EDGE ( 'NONE', *, *, #57173, .T. ) ;
#13272=LINE ( 'NONE', #47608, #46746 ) ;
#13321=DIRECTION ( 'NONE',  ( 1.000000000000000000, 0.000000000000000000, 0.000000000000000000 ) ) ;
#13461=ORIENTED_EDGE ( 'NONE', *, *, #4625, .F. ) ;
#13500=ORIENTED_EDGE ( 'NONE', *, *, #11098, .T. ) ;
#13784=CARTESIAN_POINT ( 'NONE',  ( -12.00000000000000000, 6.928203230275504332, -14.00000000000000178 ) ) ;
#13786=ADVANCED_FACE ( 'NONE', ( #51530 ), #68513, .F. ) ;
#13893=ADVANCED_FACE ( 'NONE', ( #57208 ), #74548, .T. ) ;
#13951=LINE ( 'NONE', #42643, #59199 ) ;
#13956=AXIS2_PLACEMENT_3D ( 'NONE', #30693, #42741, #25385 ) ;
#14113=DIRECTION ( 'NONE',  ( 0.8660254037844377084, -0.5000000000000017764, 0.000000000000000000 ) ) ;
#14308=CARTESIAN_POINT ( 'NONE',  ( 0.000000000000000000, 0.000000000000000000, -14.00000000000000178 ) ) ;
#14435=DIRECTION ( 'NONE',  ( -0.000000000000000000, -0.000000000000000000, 1.000000000000000000 ) ) ;
#14459=EDGE_LOOP ( 'NONE', ( #34655, #23393 ) ) ;
#14662=DIRECTION ( 'NONE',  ( 0.000000000000000000, -0.000000000000000000, 1.000000000000000000 ) ) ;
#14707=CARTESIAN_POINT ( 'NONE',  ( 6.000000000000029310, -10.39230484541328714, -14.00000000000000178 ) ) ;
#14821=ORIENTED_EDGE ( 'NONE', *, *, #6304, .F. ) ;
#14843=CARTESIAN_POINT ( 'NONE',  ( 0.000000000000000000, 0.000000000000000000, -14.80000000000000071 ) ) ;
#14922=DIRECTION ( 'NONE',  ( -0.000000000000000000, -0.000000000000000000, 1.000000000000000000 ) ) ;
#14936=EDGE_CURVE ( 'NONE', #47682, #72263, #22540, .T. ) ;
#15028=EDGE_CURVE ( 'NONE', #72263, #73846, #54899, .T. ) ;
#15035=DIRECTION ( 'NONE',  ( 1.000000000000000000, 0.000000000000000000, 0.000000000000000000 ) ) ;
#15107=CARTESIAN_POINT ( 'NONE',  ( -12.00000000000000000, -6.928203230275542523, -1.071796769724504550 ) ) ;
#15150=CARTESIAN_POINT ( 'NONE',  ( -8.031737012268317599, 9.219280934457623644, -0.1021479564361138237 ) ) ;
#15222=VERTEX_POINT ( 'NONE', #46715 ) ;
#15255=CARTESIAN_POINT ( 'NONE',  ( -6.000000000000015099, 10.39230484541326227, -14.00000000000000178 ) ) ;
#15295=DIRECTION ( 'NONE',  ( 1.000000000000000000, 0.000000000000000000, 0.000000000000000000 ) ) ;
#15484=CIRCLE ( 'NONE', #51644, 7.000000000000000000 ) ;
#15521=DIRECTION ( 'NONE',  ( -0.000000000000000000, -0.000000000000000000, 1.000000000000000000 ) ) ;
#15540=CARTESIAN_POINT ( 'NONE',  ( -12.00000000000000178, 2.352228297136951252, -0.1238145317436992882 ) ) ;
#15608=CARTESIAN_POINT ( 'NONE',  ( -12.00000000000000000, -6.928203230275527424, -14.00000000000000178 ) ) ;
#15638=CARTESIAN_POINT ( 'NONE',  ( 12.00000000000000355, -6.928203230275539859, -1.071796769724504550 ) ) ;
#15640=AXIS2_PLACEMENT_3D ( 'NONE', #68775, #69526, #29534 ) ;
#15649=CARTESIAN_POINT ( 'NONE',  ( -4.977777815167797826, -10.98248509899778291, -1.005597514980305363E-14 ) ) ;
#15689=CARTESIAN_POINT ( 'NONE',  ( -8.000000000000005329, 0.000000000000000000, -14.77459999999999951 ) ) ;
#15788=EDGE_CURVE ( 'NONE', #72148, #19, #74563, .T. ) ;
#15791=ORIENTED_EDGE ( 'NONE', *, *, #34820, .F. ) ;
#15949=AXIS2_PLACEMENT_3D ( 'NONE', #9209, #44661, #45035 ) ;
#16108=CARTESIAN_POINT ( 'NONE',  ( 6.000000000000011546, -10.39230484541325694, 0.000000000000000000 ) ) ;
#16257=CARTESIAN_POINT ( 'NONE',  ( 12.00000000000000000, 6.928203230275491009, -14.00000000000000178 ) ) ;
#16320=ORIENTED_EDGE ( 'NONE', *, *, #21579, .T. ) ;
#16611=EDGE_CURVE ( 'NONE', #53065, #54420, #35120, .T. ) ;
#16706=FACE_OUTER_BOUND ( 'NONE', #31240, .T. ) ;
#16806=DIRECTION ( 'NONE',  ( -1.000000000000000000, 0.000000000000000000, 0.000000000000000000 ) ) ;
#16952=DIRECTION ( 'NONE',  ( 0.000000000000000000, 0.000000000000000000, -1.000000000000000000 ) ) ;
#17012=LINE ( 'NONE', #40775, #68057 ) ;
#17045=EDGE_LOOP ( 'NONE', ( #52885, #58915, #1649, #30603, #6543, #13500 ) ) ;
#17066=ORIENTED_EDGE ( 'NONE', *, *, #64167, .F. ) ;
#17152=CONICAL_SURFACE ( 'NONE', #36444, 8.000000000000005329, 0.9599310885968794782 ) ;
#17215=ORIENTED_EDGE ( 'NONE', *, *, #16611, .T. ) ;
#17237=DIRECTION ( 'NONE',  ( 0.5000000000000009992, -0.8660254037844380415, 0.000000000000000000 ) ) ;
#17261=EDGE_CURVE ( 'NONE', #34052, #6656, #13951, .T. ) ;
#17294=DIRECTION ( 'NONE',  ( -1.000000000000000000, 0.000000000000000000, 0.000000000000000000 ) ) ;
#17375=CARTESIAN_POINT ( 'NONE',  ( 12.00000000000000178, -2.333919766284219488, -0.1006330532450328968 ) ) ;
#17453=CARTESIAN_POINT ( 'NONE',  ( -1.734723475976807094E-15, 13.85640646055103886, -14.80000000000000071 ) ) ;
#17465=B_SPLINE_CURVE_WITH_KNOTS ( 'NONE', 3,
 ( #43964, #21318, #66973, #32284, #15649, #55298 ),
 .UNSPECIFIED., .F., .F.,
 ( 4, 2, 4 ),
 ( 2.380729646213380196E-07, 0.003505341553885911888, 0.007010445034807201957 ),
 .UNSPECIFIED. ) ;
#17682=CARTESIAN_POINT ( 'NONE',  ( 0.000000000000000000, 23.85640646055104241, -14.00000000000000178 ) ) ;
#17776=( GEOMETRIC_REPRESENTATION_CONTEXT ( 3 ) GLOBAL_UNCERTAINTY_ASSIGNED_CONTEXT ( ( #40812 ) ) GLOBAL_UNIT_ASSIGNED_CONTEXT ( ( #11085, #27682, #63126 ) ) REPRESENTATION_CONTEXT ( 'NONE', 'WORKASPACE' ) );
#17866=DIRECTION ( 'NONE',  ( -1.000000000000000000, 0.000000000000000000, 0.000000000000000000 ) ) ;
#17914=CONICAL_SURFACE ( 'NONE', #8256, 12.00000000000000000, 1.047197551196596077 ) ;
#17996=CARTESIAN_POINT ( 'NONE',  ( 0.000000000000000000, 0.000000000000000000, 0.000000000000000000 ) ) ;
#18039=DIRECTION ( 'NONE',  ( -0.000000000000000000, -0.000000000000000000, 1.000000000000000000 ) ) ;
#18527=AXIS2_PLACEMENT_3D ( 'NONE', #53356, #47670, #48413 ) ;
#18619=CARTESIAN_POINT ( 'NONE',  ( 0.000000000000000000, 0.000000000000000000, -14.00000000000000178 ) ) ;
#18626=EDGE_CURVE ( 'NONE', #15222, #20958, #66431, .T. ) ;
#18731=EDGE_LOOP ( 'NONE', ( #37633, #21365, #71233 ) ) ;
#18753=ORIENTED_EDGE ( 'NONE', *, *, #48982, .T. ) ;
#18874=LINE ( 'NONE', #2263, #41560 ) ;
#18925=AXIS2_PLACEMENT_3D ( 'NONE', #23126, #63489, #40484 ) ;
#18980=VERTEX_POINT ( 'NONE', #28513 ) ;
#18998=PLANE ( 'NONE',  #13956 ) ;
#19057=VECTOR ( 'NONE', #51539, 1000.000000000000000 ) ;
#19258=FACE_OUTER_BOUND ( 'NONE', #21774, .T. ) ;
#19412=AXIS2_PLACEMENT_3D ( 'NONE', #18619, #1288, #919 ) ;
#19458=VECTOR ( 'NONE', #5523, 1000.000000000000114 ) ;
#19501=EDGE_CURVE ( 'NONE', #3350, #57691, #39292, .T. ) ;
#19514=ORIENTED_EDGE ( 'NONE', *, *, #59781, .T. ) ;
#19686=EDGE_CURVE ( 'NONE', #56610, #52340, #63605, .T. ) ;
#19743=PRODUCT_DEFINITION_SHAPE ( 'NONE', 'NONE',  #43127 ) ;
#19757=ORIENTED_EDGE ( 'NONE', *, *, #47311, .F. ) ;
#19759=LINE ( 'NONE', #25779, #40007 ) ;
#19893=EDGE_LOOP ( 'NONE', ( #52078, #13215, #18753, #10489, #35867, #2835 ) ) ;
#20078=ORIENTED_EDGE ( 'NONE', *, *, #7139, .T. ) ;
#20138=FACE_OUTER_BOUND ( 'NONE', #48314, .T. ) ;
#20221=DIRECTION ( 'NONE',  ( -0.000000000000000000, -0.000000000000000000, 1.000000000000000000 ) ) ;
#20237=DIRECTION ( 'NONE',  ( 1.000000000000000000, 0.000000000000000000, 0.000000000000000000 ) ) ;
#20293=ORIENTED_EDGE ( 'NONE', *, *, #67828, .F. ) ;
#20358=EDGE_LOOP ( 'NONE', ( #51200, #8076, #43279, #43326, #6960, #42899 ) ) ;
#20366=PLANE ( 'NONE',  #64019 ) ;
#20385=VECTOR ( 'NONE', #9055, 1000.000000000000000 ) ;
#20405=ORIENTED_EDGE ( 'NONE', *, *, #20935, .T. ) ;
#20688=FACE_OUTER_BOUND ( 'NONE', #35157, .T. ) ;
#20749=DIRECTION ( 'NONE',  ( -0.000000000000000000, -0.000000000000000000, 1.000000000000000000 ) ) ;
#20781=AXIS2_PLACEMENT_3D ( 'NONE', #14308, #36971, #8293 ) ;
#20817=EDGE_LOOP ( 'NONE', ( #41390, #31892, #61691 ) ) ;
#20824=CARTESIAN_POINT ( 'NONE',  ( 0.000000000000000000, 0.000000000000000000, -14.80000000000000071 ) ) ;
#20834=ORIENTED_EDGE ( 'NONE', *, *, #14936, .T. ) ;
#20839=LINE ( 'NONE', #67252, #57370 ) ;
#20935=EDGE_CURVE ( 'NONE', #20958, #53065, #19759, .T. ) ;
#20958=VERTEX_POINT ( 'NONE', #2418 ) ;
#21268=CARTESIAN_POINT ( 'NONE',  ( 12.00000000000000000, 6.928203230275491009, -14.00000000000000178 ) ) ;
#21307=CARTESIAN_POINT ( 'NONE',  ( 7.022222184832267011, -9.802124591828780709, -1.180763928472494673E-14 ) ) ;
#21318=CARTESIAN_POINT ( 'NONE',  ( -0.9815212833345903221, -13.28972488340249214, -0.7446230086126913728 ) ) ;
#21340=CARTESIAN_POINT ( 'NONE',  ( 0.000000000000000000, 0.000000000000000000, -14.77459999999999951 ) ) ;
#21365=ORIENTED_EDGE ( 'NONE', *, *, #19686, .F. ) ;
#21469=B_SPLINE_CURVE_WITH_KNOTS ( 'NONE', 3,
 ( #26481, #21576, #72137, #15540, #38581, #60826, #44603, #67616 ),
 .UNSPECIFIED., .F., .F.,
 ( 4, 2, 2, 4 ),
 ( 0.01936970057594187763, 0.02112296051615076067, 0.02287622045635964371, 0.02638274033677740979 ),
 .UNSPECIFIED. ) ;
#21470=CARTESIAN_POINT ( 'NONE',  ( -12.00000000000000178, -4.647306338817279503, -0.4736860157878169386 ) ) ;
#21543=VERTEX_POINT ( 'NONE', #26435 ) ;
#21559=CARTESIAN_POINT ( 'NONE',  ( -12.00000000000000000, 6.928203230275504332, -1.071796769724504550 ) ) ;
#21576=CARTESIAN_POINT ( 'NONE',  ( -11.99999999999999822, 0.5857239961182026944, 7.623296525288699970E-18 ) ) ;
#21579=EDGE_CURVE ( 'NONE', #29704, #70940, #60032, .T. ) ;
#21587=ORIENTED_EDGE ( 'NONE', *, *, #36658, .F. ) ;
#21774=EDGE_LOOP ( 'NONE', ( #62267, #71910, #28289 ) ) ;
#21793=CIRCLE ( 'NONE', #60368, 12.00000000000000000 ) ;
#21985=CIRCLE ( 'NONE', #11025, 12.00000000000000000 ) ;
#22045=VERTEX_POINT ( 'NONE', #15689 ) ;
#22179=ORIENTED_EDGE ( 'NONE', *, *, #51458, .F. ) ;
#22244=ORIENTED_EDGE ( 'NONE', *, *, #70810, .T. ) ;
#22404=CARTESIAN_POINT ( 'NONE',  ( 6.000000000000023093, 10.39230484541324984, 0.000000000000000000 ) ) ;
#22540=B_SPLINE_CURVE_WITH_KNOTS ( 'NONE', 3,
 ( #37724, #44127, #43359, #72796, #27136, #38097 ),
 .UNSPECIFIED., .F., .F.,
 ( 4, 2, 4 ),
 ( 2.380729645507424821E-07, 0.003505341553885866785, 0.007010445034807182875 ),
 .UNSPECIFIED. ) ;
#22559=DIRECTION ( 'NONE',  ( -0.8660254037844374864, 0.5000000000000018874, 0.000000000000000000 ) ) ;
#22738=ADVANCED_FACE ( 'NONE', ( #20138 ), #50380, .F. ) ;
#22857=CARTESIAN_POINT ( 'NONE',  ( 0.000000000000000000, 0.000000000000000000, 0.000000000000000000 ) ) ;
#22942=ADVANCED_FACE ( 'NONE', ( #16706 ), #51056, .T. ) ;
#23117=AXIS2_PLACEMENT_3D ( 'NONE', #66018, #2281, #46911 ) ;
#23126=CARTESIAN_POINT ( 'NONE',  ( 5.841566664369303132E-15, 13.85640646055103531, -14.80000000000000071 ) ) ;
#23217=CIRCLE ( 'NONE', #20781, 12.00000000000000178 ) ;
#23247=ORIENTED_EDGE ( 'NONE', *, *, #45465, .F. ) ;
#23291=EDGE_CURVE ( 'NONE', #55580, #54420, #23496, .T. ) ;
#23393=ORIENTED_EDGE ( 'NONE', *, *, #18626, .F. ) ;
#23424=ORIENTED_EDGE ( 'NONE', *, *, #19501, .F. ) ;
#23437=DIRECTION ( 'NONE',  ( -1.000000000000000000, 0.000000000000000000, 0.000000000000000000 ) ) ;
#23440=ORIENTED_EDGE ( 'NONE', *, *, #71294, .F. ) ;
#23496=LINE ( 'NONE', #69529, #3326 ) ;
#23638=ORIENTED_EDGE ( 'NONE', *, *, #1996, .F. ) ;
#23697=CONICAL_SURFACE ( 'NONE', #46579, 12.00000000000000000, 1.047197551196596077 ) ;
#23741=ORIENTED_EDGE ( 'NONE', *, *, #15028, .F. ) ;
#23806=CARTESIAN_POINT ( 'NONE',  ( 12.00000000000000000, 2.937369556047708219, -0.1973350489338391855 ) ) ;
#24139=AXIS2_PLACEMENT_3D ( 'NONE', #67097, #38431, #49358 ) ;
#24148=DIRECTION ( 'NONE',  ( -1.000000000000000000, 0.000000000000000000, 0.000000000000000000 ) ) ;
#24172=ADVANCED_FACE ( 'NONE', ( #31400 ), #48742, .F. ) ;
#24568=VECTOR ( 'NONE', #67465, 1000.000000000000114 ) ;
#24654=CARTESIAN_POINT ( 'NONE',  ( -12.00000000000000000, 0.000000000000000000, 0.000000000000000000 ) ) ;
#24704=EDGE_CURVE ( 'NONE', #5379, #73846, #30169, .T. ) ;
#24767=DIRECTION ( 'NONE',  ( -1.000000000000000000, 0.000000000000000000, -0.000000000000000000 ) ) ;
#24772=LINE ( 'NONE', #65880, #71073 ) ;
#24787=CARTESIAN_POINT ( 'NONE',  ( 0.000000000000000000, 0.000000000000000000, -14.07439246179028203 ) ) ;
#24807=CARTESIAN_POINT ( 'NONE',  ( 5.841566664369303132E-15, 13.85640646055103531, -14.00000000000000178 ) ) ;
#25011=CARTESIAN_POINT ( 'NONE',  ( 0.000000000000000000, 0.000000000000000000, 3.469446951953614189E-15 ) ) ;
#25086=ORIENTED_EDGE ( 'NONE', *, *, #4638, .F. ) ;
#25139=CARTESIAN_POINT ( 'NONE',  ( -3.464965446656449899, 11.85590772719117503, -0.1959795092987741960 ) ) ;
#25261=DIRECTION ( 'NONE',  ( -1.000000000000000000, 1.776356839400250465E-15, 0.000000000000000000 ) ) ;
#25283=DIRECTION ( 'NONE',  ( -0.8191520442889885789, 1.003171929053520802E-16, 0.5735764363510507113 ) ) ;
#25320=CARTESIAN_POINT ( 'NONE',  ( -12.00000000000000000, -6.928203230275527424, -14.00000000000000178 ) ) ;
#25330=ORIENTED_EDGE ( 'NONE', *, *, #15028, .T. ) ;
#25385=DIRECTION ( 'NONE',  ( -1.000000000000000000, 0.000000000000000000, -0.000000000000000000 ) ) ;
#25666=ORIENTED_EDGE ( 'NONE', *, *, #6413, .T. ) ;
#25689=DIRECTION ( 'NONE',  ( 0.8660254037844377084, -0.5000000000000017764, 0.000000000000000000 ) ) ;
#25779=CARTESIAN_POINT ( 'NONE',  ( 12.00000000000000355, 0.000000000000000000, 0.000000000000000000 ) ) ;
#26007=ADVANCED_FACE ( 'NONE', ( #29580 ), #61333, .T. ) ;
#26069=ORIENTED_EDGE ( 'NONE', *, *, #39546, .F. ) ;
#26070=DIRECTION ( 'NONE',  ( -1.000000000000000000, 0.000000000000000000, 0.000000000000000000 ) ) ;
#26129=VECTOR ( 'NONE', #25689, 999.9999999999998863 ) ;
#26153=VERTEX_POINT ( 'NONE', #1122 ) ;
#26435=CARTESIAN_POINT ( 'NONE',  ( -12.00000000000000000, 6.928203230275504332, -1.071796769724504550 ) ) ;
#26462=CARTESIAN_POINT ( 'NONE',  ( -10.02978802437156425, 8.065705644765211346, -0.4750804646944142839 ) ) ;
#26481=CARTESIAN_POINT ( 'NONE',  ( -12.00000000000000000, 0.000000000000000000, 0.000000000000000000 ) ) ;
#26925=DIRECTION ( 'NONE',  ( 1.000000000000000000, 0.000000000000000000, 0.000000000000000000 ) ) ;
#26986=DIRECTION ( 'NONE',  ( 1.000000000000000000, 0.000000000000000000, 0.000000000000000000 ) ) ;
#26995=AXIS2_PLACEMENT_3D ( 'NONE', #69325, #52352, #24767 ) ;
#27093=CARTESIAN_POINT ( 'NONE',  ( -3.255014963930524218E-15, -13.85640646055106728, -14.00000000000000178 ) ) ;
#27125=CARTESIAN_POINT ( 'NONE',  ( -1.734723475976807094E-15, 13.85640646055103886, 0.000000000000000000 ) ) ;
#27136=CARTESIAN_POINT ( 'NONE',  ( 4.977777815167777398, 10.98248509899775982, 6.901624454228039163E-15 ) ) ;
#27219=ORIENTED_EDGE ( 'NONE', *, *, #3951, .F. ) ;
#27234=CARTESIAN_POINT ( 'NONE',  ( 0.000000000000000000, 0.000000000000000000, -0.7702282920306856573 ) ) ;
#27271=( GEOMETRIC_REPRESENTATION_CONTEXT ( 3 ) GLOBAL_UNCERTAINTY_ASSIGNED_CONTEXT ( ( #35839 ) ) GLOBAL_UNIT_ASSIGNED_CONTEXT ( ( #53915, #30163, #47134 ) ) REPRESENTATION_CONTEXT ( 'NONE', 'WORKASPACE' ) );
#27290=CONICAL_SURFACE ( 'NONE', #64675, 12.00000000000000000, 1.047197551196596077 ) ;
#27591=CARTESIAN_POINT ( 'NONE',  ( -11.01847871666547185, 7.494884807424044837, -0.7446230086126799375 ) ) ;
#27642=CARTESIAN_POINT ( 'NONE',  ( -3.469446951953614189E-15, -13.85640646055106728, -14.00000000000000178 ) ) ;
#27662=EDGE_CURVE ( 'NONE', #62682, #39861, #64636, .T. ) ;
#27676=DIRECTION ( 'NONE',  ( 0.000000000000000000, -1.000000000000000000, 0.000000000000000000 ) ) ;
#27682=( NAMED_UNIT ( * ) PLANE_ANGLE_UNIT ( ) SI_UNIT ( $, .RADIAN. ) );
#27703=ORIENTED_EDGE ( 'NONE', *, *, #28909, .F. ) ;
#27831=ORIENTED_EDGE ( 'NONE', *, *, #74034, .F. ) ;
#27857=DIRECTION ( 'NONE',  ( -0.000000000000000000, -0.000000000000000000, 1.000000000000000000 ) ) ;
#28289=ORIENTED_EDGE ( 'NONE', *, *, #58364, .T. ) ;
#28383=CARTESIAN_POINT ( 'NONE',  ( -12.00000000000000000, -6.928203230275527424, -14.80000000000000071 ) ) ;
#28513=CARTESIAN_POINT ( 'NONE',  ( 7.000000000000000000, 0.000000000000000000, -0.7002075382097148193 ) ) ;
#28515=PLANE ( 'NONE',  #31207 ) ;
#28531=LINE ( 'NONE', #34214, #19057 ) ;
#28595=ORIENTED_EDGE ( 'NONE', *, *, #74467, .T. ) ;
#28629=CARTESIAN_POINT ( 'NONE',  ( 8.535034553343558983, 8.928701963635351291, -0.1959795092987683951 ) ) ;
#28909=EDGE_CURVE ( 'NONE', #19, #3350, #12862, .T. ) ;
#29011=B_SPLINE_CURVE_WITH_KNOTS ( 'NONE', 3,
 ( #60389, #37770, #59657, #2308, #8714, #43027, #42291, #15107 ),
 .UNSPECIFIED., .F., .F.,
 ( 4, 2, 2, 4 ),
 ( 0.007010445034807201957, 0.008756443665256739492, 0.01050244229570627269, 0.01399443955660533909 ),
 .UNSPECIFIED. ) ;
#29037=VECTOR ( 'NONE', #14113, 999.9999999999998863 ) ;
#29134=PLANE ( 'NONE',  #67876 ) ;
#29290=ORIENTED_EDGE ( 'NONE', *, *, #23291, .F. ) ;
#29361=DIRECTION ( 'NONE',  ( 0.5000000000000019984, 0.8660254037844375974, -0.000000000000000000 ) ) ;
#29457=DIRECTION ( 'NONE',  ( 0.000000000000000000, 0.000000000000000000, -1.000000000000000000 ) ) ;
#29482=ORIENTED_EDGE ( 'NONE', *, *, #10147, .T. ) ;
#29485=PLANE ( 'NONE',  #57046 ) ;
#29534=DIRECTION ( 'NONE',  ( 1.000000000000000000, 0.000000000000000000, 0.000000000000000000 ) ) ;
#29580=FACE_OUTER_BOUND ( 'NONE', #18731, .T. ) ;
#29636=CARTESIAN_POINT ( 'NONE',  ( 12.00000000000000000, 6.928203230275491009, -14.80000000000000071 ) ) ;
#29680=ORIENTED_EDGE ( 'NONE', *, *, #21579, .F. ) ;
#29704=VERTEX_POINT ( 'NONE', #15608 ) ;
#29819=CARTESIAN_POINT ( 'NONE',  ( 12.00000000000000000, 0.000000000000000000, 0.000000000000000000 ) ) ;
#29828=CARTESIAN_POINT ( 'NONE',  ( 5.490800045006650976, -10.68629157650006256, -1.191902411728888722E-14 ) ) ;
#29844=ADVANCED_FACE ( 'NONE', ( #58147 ), #72257, .T. ) ;
#29871=EDGE_LOOP ( 'NONE', ( #59456, #17215, #29290 ) ) ;
#30036=FACE_OUTER_BOUND ( 'NONE', #64565, .T. ) ;
#30053=PLANE ( 'NONE',  #71746 ) ;
#30163=( NAMED_UNIT ( * ) PLANE_ANGLE_UNIT ( ) SI_UNIT ( $, .RADIAN. ) );
#30169=B_SPLINE_CURVE_WITH_KNOTS ( 'NONE', 3,
 ( #42254, #6828, #36609, #65266, #23806, #46809, #70568, #69833 ),
 .UNSPECIFIED., .F., .F.,
 ( 4, 2, 2, 4 ),
 ( 0.01936970057594189498, 0.02112296051615078496, 0.02287622045635967841, 0.02638274033677746183 ),
 .UNSPECIFIED. ) ;
#30296=DIRECTION ( 'NONE',  ( 0.000000000000000000, 0.000000000000000000, 1.000000000000000000 ) ) ;
#30335=CARTESIAN_POINT ( 'NONE',  ( -6.000000000000021316, -10.39230484541325161, 0.000000000000000000 ) ) ;
#30530=EDGE_CURVE ( 'NONE', #68303, #62350, #12104, .T. ) ;
#30603=ORIENTED_EDGE ( 'NONE', *, *, #11437, .F. ) ;
#30693=CARTESIAN_POINT ( 'NONE',  ( 0.000000000000000000, 23.85640646055104241, -14.00000000000000178 ) ) ;
#30792=CIRCLE ( 'NONE', #3055, 12.00000000000000178 ) ;
#30832=ADVANCED_FACE ( 'NONE', ( #60825 ), #8493, .F. ) ;
#30928=DIRECTION ( 'NONE',  ( 0.000000000000000000, 0.000000000000000000, 1.000000000000000000 ) ) ;
#30985=LINE ( 'NONE', #60025, #51489 ) ;
#31185=CARTESIAN_POINT ( 'NONE',  ( -3.967492730755044494, 11.56577346444171717, -0.1233701403699368204 ) ) ;
#31207=AXIS2_PLACEMENT_3D ( 'NONE', #29636, #16806, #69629 ) ;
#31229=DIRECTION ( 'NONE',  ( 0.000000000000000000, 0.000000000000000000, -1.000000000000000000 ) ) ;
#31240=EDGE_LOOP ( 'NONE', ( #7081, #22244, #36265, #64680, #45797, #57433 ) ) ;
#31343=CIRCLE ( 'NONE', #61515, 8.000000000000005329 ) ;
#31400=FACE_OUTER_BOUND ( 'NONE', #63103, .T. ) ;
#31598=LINE ( 'NONE', #24807, #43688 ) ;
#31892=ORIENTED_EDGE ( 'NONE', *, *, #73203, .T. ) ;
#32081=FACE_OUTER_BOUND ( 'NONE', #11196, .T. ) ;
#32284=CARTESIAN_POINT ( 'NONE',  ( -3.968262987731734359, -11.56532875636891156, -0.1021479564361298803 ) ) ;
#32341=DIRECTION ( 'NONE',  ( 1.000000000000000000, 0.000000000000000000, 0.000000000000000000 ) ) ;
#32472=AXIS2_PLACEMENT_3D ( 'NONE', #52126, #458, #23437 ) ;
#32549=DIRECTION ( 'NONE',  ( 1.000000000000000000, 0.000000000000000000, 0.000000000000000000 ) ) ;
#32605=CIRCLE ( 'NONE', #7290, 8.000000000000003553 ) ;
#32626=FACE_OUTER_BOUND ( 'NONE', #41770, .T. ) ;
#32672=CARTESIAN_POINT ( 'NONE',  ( 0.000000000000000000, 0.000000000000000000, -14.77459999999999951 ) ) ;
#32772=EDGE_LOOP ( 'NONE', ( #70808, #74232, #13461 ) ) ;
#32859=EDGE_LOOP ( 'NONE', ( #51528, #69793, #20078, #7597 ) ) ;
#32871=ORIENTED_EDGE ( 'NONE', *, *, #48982, .F. ) ;
#32911=CARTESIAN_POINT ( 'NONE',  ( -6.000000000000012434, 10.39230484541325694, 0.000000000000000000 ) ) ;
#33356=PLANE ( 'NONE',  #15949 ) ;
#34052=VERTEX_POINT ( 'NONE', #50830 ) ;
#34077=AXIS2_PLACEMENT_3D ( 'NONE', #71655, #9423, #25261 ) ;
#34214=CARTESIAN_POINT ( 'NONE',  ( -12.00000000000000000, 6.928203230275504332, -14.80000000000000071 ) ) ;
#34366=CARTESIAN_POINT ( 'NONE',  ( 5.841566664369303132E-15, 13.85640646055103531, -14.00000000000000178 ) ) ;
#34459=DIRECTION ( 'NONE',  ( 1.000000000000000000, 0.000000000000000000, 0.000000000000000000 ) ) ;
#34553=EDGE_CURVE ( 'NONE', #68525, #26153, #2244, .T. ) ;
#34618=ORIENTED_EDGE ( 'NONE', *, *, #39546, .T. ) ;
#34655=ORIENTED_EDGE ( 'NONE', *, *, #74388, .F. ) ;
#34820=EDGE_CURVE ( 'NONE', #68303, #18980, #39186, .T. ) ;
#34874=CARTESIAN_POINT ( 'NONE',  ( 0.000000000000000000, 0.000000000000000000, -14.07439246179028203 ) ) ;
#35061=DIRECTION ( 'NONE',  ( -1.000000000000000000, 0.000000000000000000, -0.000000000000000000 ) ) ;
#35073=ORIENTED_EDGE ( 'NONE', *, *, #74388, .T. ) ;
#35120=CIRCLE ( 'NONE', #19412, 12.00000000000000178 ) ;
#35157=EDGE_LOOP ( 'NONE', ( #12529, #42918, #5661, #46493 ) ) ;
#35211=AXIS2_PLACEMENT_3D ( 'NONE', #55749, #31229, #44416 ) ;
#35227=EDGE_CURVE ( 'NONE', #62350, #68303, #15484, .T. ) ;
#35719=FACE_OUTER_BOUND ( 'NONE', #17045, .T. ) ;
#35839=UNCERTAINTY_MEASURE_WITH_UNIT (LENGTH_MEASURE( 1.000000000000000082E-05 ), #53915, 'distance_accuracy_value', 'NONE');
#35867=ORIENTED_EDGE ( 'NONE', *, *, #45465, .T. ) ;
#35942=CARTESIAN_POINT ( 'NONE',  ( 8.000000000000000000, 0.000000000000000000, 3.577867169202164632E-15 ) ) ;
#36231=CARTESIAN_POINT ( 'NONE',  ( 1.966308894373107963, -12.72115749107479310, -0.4760262082327907929 ) ) ;
#36265=ORIENTED_EDGE ( 'NONE', *, *, #4625, .T. ) ;
#36340=ORIENTED_EDGE ( 'NONE', *, *, #36658, .T. ) ;
#36351=AXIS2_PLACEMENT_3D ( 'NONE', #6772, #46748, #46383 ) ;
#36444=AXIS2_PLACEMENT_3D ( 'NONE', #69659, #46639, #52312 ) ;
#36484=CARTESIAN_POINT ( 'NONE',  ( -1.966308894373119287, 12.72115749107475402, -0.4760262082327688105 ) ) ;
#36609=CARTESIAN_POINT ( 'NONE',  ( 12.00000000000000178, 1.173324140324976783, -0.02489140746004406615 ) ) ;
#36658=EDGE_CURVE ( 'NONE', #62350, #34052, #20839, .T. ) ;
#36829=DIRECTION ( 'NONE',  ( 0.000000000000000000, -1.000000000000000000, 0.000000000000000000 ) ) ;
#36933=PRODUCT_CONTEXT ( 'NONE', #64545, 'mechanical' ) ;
#36971=DIRECTION ( 'NONE',  ( -0.000000000000000000, -0.000000000000000000, 1.000000000000000000 ) ) ;
#37007=ORIENTED_EDGE ( 'NONE', *, *, #34820, .T. ) ;
#37262=CARTESIAN_POINT ( 'NONE',  ( 0.000000000000000000, 23.85640646055104241, -14.00000000000000178 ) ) ;
#37361=VERTEX_POINT ( 'NONE', #5653 ) ;
#37509=ADVANCED_FACE ( 'NONE', ( #53157 ), #23697, .T. ) ;
#37633=ORIENTED_EDGE ( 'NONE', *, *, #57173, .F. ) ;
#37669=CIRCLE ( 'NONE', #43619, 8.000000000000000000 ) ;
#37724=CARTESIAN_POINT ( 'NONE',  ( 7.806255641895631925E-15, 13.85640646055103709, -1.071796769724504550 ) ) ;
#37770=CARTESIAN_POINT ( 'NONE',  ( -6.509199954993407644, -10.09831811432650817, -1.016439536705163562E-14 ) ) ;
#37771=ADVANCED_FACE ( 'NONE', ( #48215 ), #27290, .T. ) ;
#37871=ORIENTED_EDGE ( 'NONE', *, *, #11437, .T. ) ;
#38097=CARTESIAN_POINT ( 'NONE',  ( 6.000000000000023093, 10.39230484541324984, 0.000000000000000000 ) ) ;
#38431=DIRECTION ( 'NONE',  ( -0.000000000000000000, -0.000000000000000000, 1.000000000000000000 ) ) ;
#38529=ORIENTED_EDGE ( 'NONE', *, *, #70810, .F. ) ;
#38580=DIRECTION ( 'NONE',  ( -0.000000000000000000, -0.000000000000000000, 1.000000000000000000 ) ) ;
#38581=CARTESIAN_POINT ( 'NONE',  ( -12.00000000000000000, 2.937369556047691788, -0.1973350489338370206 ) ) ;
#38714=EDGE_CURVE ( 'NONE', #48595, #62682, #30985, .T. ) ;
#38832=DIRECTION ( 'NONE',  ( 0.000000000000000000, 0.000000000000000000, -1.000000000000000000 ) ) ;
#39084=CARTESIAN_POINT ( 'NONE',  ( 6.900000000000001243, 0.000000000000000000, -0.7702282920306856573 ) ) ;
#39180=FACE_OUTER_BOUND ( 'NONE', #3603, .T. ) ;
#39186=LINE ( 'NONE', #45217, #39584 ) ;
#39204=CARTESIAN_POINT ( 'NONE',  ( -12.00000000000000000, -6.928203230275542523, -1.071796769724504550 ) ) ;
#39266=ORIENTED_EDGE ( 'NONE', *, *, #5361, .T. ) ;
#39292=B_SPLINE_CURVE_WITH_KNOTS ( 'NONE', 3,
 ( #1895, #29828, #1173, #13192, #11732, #36231, #12828, #59247 ),
 .UNSPECIFIED., .F., .F.,
 ( 4, 2, 2, 4 ),
 ( 0.007010445034807124762, 0.008756443665256687450, 0.01050244229570624840, 0.01399443955660537552 ),
 .UNSPECIFIED. ) ;
#39546=EDGE_CURVE ( 'NONE', #18980, #42139, #43614, .T. ) ;
#39584=VECTOR ( 'NONE', #51246, 1000.000000000000000 ) ;
#39789=AXIS2_PLACEMENT_3D ( 'NONE', #22857, #74170, #50788 ) ;
#39843=DIRECTION ( 'NONE',  ( 1.000000000000000000, 0.000000000000000000, 0.000000000000000000 ) ) ;
#39861=VERTEX_POINT ( 'NONE', #2055 ) ;
#40007=VECTOR ( 'NONE', #54487, 1000.000000000000000 ) ;
#40373=MANIFOLD_SOLID_BREP ( 'EndChamfer', #10549 ) ;
#40484=DIRECTION ( 'NONE',  ( -0.8660254037844380415, -0.5000000000000011102, 0.000000000000000000 ) ) ;
#40547=DIRECTION ( 'NONE',  ( -0.000000000000000000, -0.000000000000000000, 1.000000000000000000 ) ) ;
#40742=ORIENTED_EDGE ( 'NONE', *, *, #74503, .F. ) ;
#40775=CARTESIAN_POINT ( 'NONE',  ( 12.00000000000000000, 6.928203230275491009, -14.00000000000000178 ) ) ;
#40812=UNCERTAINTY_MEASURE_WITH_UNIT (LENGTH_MEASURE( 1.000000000000000082E-05 ), #11085, 'distance_accuracy_value', 'NONE');
#41052=ORIENTED_EDGE ( 'NONE', *, *, #17261, .F. ) ;
#41230=DIRECTION ( 'NONE',  ( -0.8660254037844374864, 0.5000000000000018874, 0.000000000000000000 ) ) ;
#41390=ORIENTED_EDGE ( 'NONE', *, *, #6413, .F. ) ;
#41560=VECTOR ( 'NONE', #30928, 1000.000000000000000 ) ;
#41593=EDGE_CURVE ( 'NONE', #62682, #21543, #28531, .T. ) ;
#41607=LINE ( 'NONE', #54042, #49542 ) ;
#41639=CARTESIAN_POINT ( 'NONE',  ( 0.000000000000000000, 0.000000000000000000, 0.000000000000000000 ) ) ;
#41769=CARTESIAN_POINT ( 'NONE',  ( -4.979315568031092099, 10.98159727696817889, -0.02533325329315395946 ) ) ;
#41770=EDGE_LOOP ( 'NONE', ( #19514, #74225, #27703 ) ) ;
#41850=ORIENTED_EDGE ( 'NONE', *, *, #74034, .T. ) ;
#42128=EDGE_CURVE ( 'NONE', #68303, #37361, #13272, .T. ) ;
#42139=VERTEX_POINT ( 'NONE', #35942 ) ;
#42254=CARTESIAN_POINT ( 'NONE',  ( 12.00000000000000000, 0.000000000000000000, 0.000000000000000000 ) ) ;
#42270=CARTESIAN_POINT ( 'NONE',  ( 0.000000000000000000, 23.85640646055104241, -14.00000000000000178 ) ) ;
#42291=CARTESIAN_POINT ( 'NONE',  ( -11.02092980224262142, -7.493469672506294366, -0.7454400371385534463 ) ) ;
#42515=ORIENTED_EDGE ( 'NONE', *, *, #27662, .T. ) ;
#42532=EDGE_LOOP ( 'NONE', ( #55876, #59612, #29680 ) ) ;
#42631=PRODUCT ( 'hexagon nut style 1_is_IS 1364-3 - M16-W-N', 'hexagon nut style 1_is_IS 1364-3 - M16-W-N', '', ( #36933 ) ) ;
#42643=CARTESIAN_POINT ( 'NONE',  ( -6.900000000000001243, 8.450062914116738633E-16, -0.7702282920306856573 ) ) ;
#42676=ORIENTED_EDGE ( 'NONE', *, *, #74503, .T. ) ;
#42703=ORIENTED_EDGE ( 'NONE', *, *, #17261, .T. ) ;
#42741=DIRECTION ( 'NONE',  ( 0.000000000000000000, 0.000000000000000000, -1.000000000000000000 ) ) ;
#42877=CYLINDRICAL_SURFACE ( 'NONE', #44654, 8.000000000000003553 ) ;
#42899=ORIENTED_EDGE ( 'NONE', *, *, #24704, .F. ) ;
#42918=ORIENTED_EDGE ( 'NONE', *, *, #63833, .T. ) ;
#43027=CARTESIAN_POINT ( 'NONE',  ( -10.03369110562688959, -8.063452199751800720, -0.4760262082327739175 ) ) ;
#43036=DIRECTION ( 'NONE',  ( -0.8660254037844380415, -0.5000000000000011102, 0.000000000000000000 ) ) ;
#43127=PRODUCT_DEFINITION ( 'UNKNOWN', '', #71904, #12441 ) ;
#43184=ADVANCED_FACE ( 'NONE', ( #55066, #55817 ), #4134, .F. ) ;
#43279=ORIENTED_EDGE ( 'NONE', *, *, #67372, .F. ) ;
#43326=ORIENTED_EDGE ( 'NONE', *, *, #71167, .F. ) ;
#43359=CARTESIAN_POINT ( 'NONE',  ( 1.970211975628451295, 12.71890404606132030, -0.4750804646944193355 ) ) ;
#43415=CIRCLE ( 'NONE', #24139, 12.00000000000000178 ) ;
#43566=CARTESIAN_POINT ( 'NONE',  ( -7.000000000000000000, 8.572527594031473190E-16, -14.07439246179028203 ) ) ;
#43614=LINE ( 'NONE', #39084, #883 ) ;
#43619=AXIS2_PLACEMENT_3D ( 'NONE', #71556, #47807, #32341 ) ;
#43688=VECTOR ( 'NONE', #47822, 1000.000000000000114 ) ;
#43707=DIRECTION ( 'NONE',  ( -0.000000000000000000, -0.000000000000000000, 1.000000000000000000 ) ) ;
#43954=CARTESIAN_POINT ( 'NONE',  ( 8.031737012268331810, -9.219280934457653842, -0.1021479564361314485 ) ) ;
#43964=CARTESIAN_POINT ( 'NONE',  ( -6.331740687315345895E-14, -13.85640646055103531, -1.071796769724504550 ) ) ;
#44127=CARTESIAN_POINT ( 'NONE',  ( 0.9815212833345395849, 13.28972488340248681, -0.7446230086126863768 ) ) ;
#44347=ADVANCED_FACE ( 'NONE', ( #48567 ), #67736, .F. ) ;
#44373=AXIS2_PLACEMENT_3D ( 'NONE', #27125, #38832, #17294 ) ;
#44416=DIRECTION ( 'NONE',  ( -1.000000000000000000, 0.000000000000000000, 0.000000000000000000 ) ) ;
#44474=AXIS2_PLACEMENT_3D ( 'NONE', #41639, #52593, #64282 ) ;
#44585=CARTESIAN_POINT ( 'NONE',  ( -7.022222184832254577, 9.802124591828755840, 6.291760732204942919E-15 ) ) ;
#44603=CARTESIAN_POINT ( 'NONE',  ( -12.00000000000000178, 5.807951393103176763, -0.7484079198486841555 ) ) ;
#44654=AXIS2_PLACEMENT_3D ( 'NONE', #65896, #48910, #20237 ) ;
#44661=DIRECTION ( 'NONE',  ( -1.000000000000000000, 0.000000000000000000, 0.000000000000000000 ) ) ;
#44691=B_SPLINE_CURVE_WITH_KNOTS ( 'NONE', 3,
 ( #7811, #65136, #41769, #31185, #25139, #36484, #70446, #53469 ),
 .UNSPECIFIED., .F., .F.,
 ( 4, 2, 2, 4 ),
 ( 0.007010445034807142976, 0.008756443665256694389, 0.01050244229570624493, 0.01399443955660534950 ),
 .UNSPECIFIED. ) ;
#44739=ADVANCED_FACE ( 'NONE', ( #30036 ), #17152, .F. ) ;
#45035=DIRECTION ( 'NONE',  ( 0.000000000000000000, 0.000000000000000000, 1.000000000000000000 ) ) ;
#45217=CARTESIAN_POINT ( 'NONE',  ( 7.000000000000000000, 0.000000000000000000, -14.80000000000000071 ) ) ;
#45298=CARTESIAN_POINT ( 'NONE',  ( 12.00000000000000000, 0.000000000000000000, 0.000000000000000000 ) ) ;
#45465=EDGE_CURVE ( 'NONE', #5379, #72263, #21985, .T. ) ;
#45495=CARTESIAN_POINT ( 'NONE',  ( 0.000000000000000000, 0.000000000000000000, -14.80000000000000071 ) ) ;
#45509=DIRECTION ( 'NONE',  ( 0.8660254037844380415, 0.5000000000000009992, 0.000000000000000000 ) ) ;
#45549=ADVANCED_FACE ( 'NONE', ( #32081 ), #20366, .T. ) ;
#45797=ORIENTED_EDGE ( 'NONE', *, *, #1996, .T. ) ;
#45823=AXIS2_PLACEMENT_3D ( 'NONE', #34874, #51080, #17866 ) ;
#45873=DIRECTION ( 'NONE',  ( 0.000000000000000000, 0.000000000000000000, 1.000000000000000000 ) ) ;
#45935=ORIENTED_EDGE ( 'NONE', *, *, #70798, .T. ) ;
#46050=CARTESIAN_POINT ( 'NONE',  ( 12.00000000000000178, -1.170752406943651902, 8.470329472542999693E-17 ) ) ;
#46355=FACE_OUTER_BOUND ( 'NONE', #29871, .T. ) ;
#46383=DIRECTION ( 'NONE',  ( -1.000000000000000000, 0.000000000000000000, 0.000000000000000000 ) ) ;
#46390=ADVANCED_FACE ( 'NONE', ( #9593 ), #33356, .T. ) ;
#46493=ORIENTED_EDGE ( 'NONE', *, *, #7139, .F. ) ;
#46579=AXIS2_PLACEMENT_3D ( 'NONE', #1491, #64478, #47106 ) ;
#46639=DIRECTION ( 'NONE',  ( 0.000000000000000000, 0.000000000000000000, -1.000000000000000000 ) ) ;
#46715=CARTESIAN_POINT ( 'NONE',  ( -12.00000000000000355, 1.469576158976824342E-15, -14.80000000000000071 ) ) ;
#46746=VECTOR ( 'NONE', #47981, 1000.000000000000114 ) ;
#46748=DIRECTION ( 'NONE',  ( 0.000000000000000000, -0.000000000000000000, 1.000000000000000000 ) ) ;
#46809=CARTESIAN_POINT ( 'NONE',  ( 11.99999999999999822, 4.673005023400526703, -0.4790896970872614014 ) ) ;
#46911=DIRECTION ( 'NONE',  ( -1.000000000000000000, 0.000000000000000000, 0.000000000000000000 ) ) ;
#46978=LINE ( 'NONE', #71455, #7388 ) ;
#47028=AXIS2_PLACEMENT_3D ( 'NONE', #67841, #43707, #10127 ) ;
#47106=DIRECTION ( 'NONE',  ( -1.000000000000000000, 0.000000000000000000, 0.000000000000000000 ) ) ;
#47134=( NAMED_UNIT ( * ) SI_UNIT ( $, .STERADIAN. ) SOLID_ANGLE_UNIT ( ) );
#47235=DIRECTION ( 'NONE',  ( -1.000000000000000000, 0.000000000000000000, 0.000000000000000000 ) ) ;
#47311=EDGE_CURVE ( 'NONE', #62350, #22045, #63592, .T. ) ;
#47415=LINE ( 'NONE', #70439, #2926 ) ;
#47608=CARTESIAN_POINT ( 'NONE',  ( 8.000000000000005329, 9.797174393178833546E-16, -14.77459999999999951 ) ) ;
#47670=DIRECTION ( 'NONE',  ( 0.000000000000000000, 0.000000000000000000, -1.000000000000000000 ) ) ;
#47682=VERTEX_POINT ( 'NONE', #70478 ) ;
#47807=DIRECTION ( 'NONE',  ( -0.000000000000000000, -0.000000000000000000, 1.000000000000000000 ) ) ;
#47822=DIRECTION ( 'NONE',  ( -0.8660254037844380415, -0.5000000000000011102, 0.000000000000000000 ) ) ;
#47981=DIRECTION ( 'NONE',  ( 0.8191520442889907994, 1.003171929053523514E-16, -0.5735764363510476027 ) ) ;
#48030=DIRECTION ( 'NONE',  ( -1.000000000000000000, 0.000000000000000000, 0.000000000000000000 ) ) ;
#48064=EDGE_CURVE ( 'NONE', #64507, #62698, #61004, .T. ) ;
#48215=FACE_OUTER_BOUND ( 'NONE', #11618, .T. ) ;
#48314=EDGE_LOOP ( 'NONE', ( #49331, #42703, #12506, #26069 ) ) ;
#48402=CARTESIAN_POINT ( 'NONE',  ( 0.000000000000000000, 0.000000000000000000, -14.80000000000000071 ) ) ;
#48413=DIRECTION ( 'NONE',  ( 1.000000000000000000, 0.000000000000000000, 0.000000000000000000 ) ) ;
#48440=DIRECTION ( 'NONE',  ( -0.000000000000000000, -0.000000000000000000, 1.000000000000000000 ) ) ;
#48539=FACE_OUTER_BOUND ( 'NONE', #32859, .T. ) ;
#48567=FACE_OUTER_BOUND ( 'NONE', #56263, .T. ) ;
#48595=VERTEX_POINT ( 'NONE', #15255 ) ;
#48611=SHAPE_DEFINITION_REPRESENTATION ( #19743, #69137 ) ;
#48742=CYLINDRICAL_SURFACE ( 'NONE', #70731, 7.000000000000000000 ) ;
#48762=CIRCLE ( 'NONE', #10217, 12.00000000000000178 ) ;
#48910=DIRECTION ( 'NONE',  ( -0.000000000000000000, -0.000000000000000000, 1.000000000000000000 ) ) ;
#48982=EDGE_CURVE ( 'NONE', #64048, #3350, #54474, .T. ) ;
#49090=MECHANICAL_DESIGN_GEOMETRIC_PRESENTATION_REPRESENTATION('',(#63549),#17776);
#49145=CARTESIAN_POINT ( 'NONE',  ( 0.000000000000000000, 0.000000000000000000, -14.00000000000000178 ) ) ;
#49180=DIRECTION ( 'NONE',  ( 0.000000000000000000, -0.000000000000000000, 1.000000000000000000 ) ) ;
#49331=ORIENTED_EDGE ( 'NONE', *, *, #56617, .T. ) ;
#49337=CARTESIAN_POINT ( 'NONE',  ( 0.000000000000000000, 0.000000000000000000, 0.000000000000000000 ) ) ;
#49358=DIRECTION ( 'NONE',  ( 1.000000000000000000, 0.000000000000000000, 0.000000000000000000 ) ) ;
#49407=AXIS2_PLACEMENT_3D ( 'NONE', #54775, #73604, #26070 ) ;
#49429=ORIENTED_EDGE ( 'NONE', *, *, #38714, .F. ) ;
#49542=VECTOR ( 'NONE', #12918, 1000.000000000000000 ) ;
#49814=ORIENTED_EDGE ( 'NONE', *, *, #23291, .T. ) ;
#50292=CARTESIAN_POINT ( 'NONE',  ( -8.000000000000003553, 9.797174393178831574E-16, -14.80000000000000071 ) ) ;
#50380=CONICAL_SURFACE ( 'NONE', #58749, 6.900000000000001243, 0.9599310885968755924 ) ;
#50548=APPLICATION_CONTEXT ( 'automotive_design' ) ;
#50648=AXIS2_PLACEMENT_3D ( 'NONE', #17453, #63479, #47235 ) ;
#50689=CARTESIAN_POINT ( 'NONE',  ( -8.000000000000000000, 9.797174393178827630E-16, 3.577867169202164632E-15 ) ) ;
#50788=DIRECTION ( 'NONE',  ( 1.000000000000000000, 0.000000000000000000, 0.000000000000000000 ) ) ;
#50830=CARTESIAN_POINT ( 'NONE',  ( -7.000000000000000000, 8.572527594031473190E-16, -0.7002075382097148193 ) ) ;
#51030=CARTESIAN_POINT ( 'NONE',  ( 12.00000000000000000, 6.928203230275491009, -14.00000000000000178 ) ) ;
#51040=CIRCLE ( 'NONE', #18527, 7.000000000000000000 ) ;
#51056=PLANE ( 'NONE',  #18925 ) ;
#51080=DIRECTION ( 'NONE',  ( -0.000000000000000000, -0.000000000000000000, 1.000000000000000000 ) ) ;
#51175=CARTESIAN_POINT ( 'NONE',  ( 12.00000000000000000, -6.928203230275538971, -14.80000000000000071 ) ) ;
#51191=ORIENTED_EDGE ( 'NONE', *, *, #42128, .F. ) ;
#51200=ORIENTED_EDGE ( 'NONE', *, *, #59781, .F. ) ;
#51246=DIRECTION ( 'NONE',  ( 0.000000000000000000, 0.000000000000000000, 1.000000000000000000 ) ) ;
#51251=ORIENTED_EDGE ( 'NONE', *, *, #4638, .T. ) ;
#51313=ORIENTED_EDGE ( 'NONE', *, *, #70879, .F. ) ;
#51392=DIRECTION ( 'NONE',  ( 0.8660254037844377084, -0.5000000000000017764, 0.000000000000000000 ) ) ;
#51400=ORIENTED_EDGE ( 'NONE', *, *, #70798, .F. ) ;
#51458=EDGE_CURVE ( 'NONE', #12103, #52340, #60590, .T. ) ;
#51489=VECTOR ( 'NONE', #43036, 1000.000000000000114 ) ;
#51528=ORIENTED_EDGE ( 'NONE', *, *, #63833, .F. ) ;
#51530=FACE_OUTER_BOUND ( 'NONE', #2353, .T. ) ;
#51539=DIRECTION ( 'NONE',  ( 0.000000000000000000, 0.000000000000000000, 1.000000000000000000 ) ) ;
#51577=DIRECTION ( 'NONE',  ( 0.000000000000000000, -0.000000000000000000, 1.000000000000000000 ) ) ;
#51641=CARTESIAN_POINT ( 'NONE',  ( 11.02092980224260543, 7.493469672506262391, -0.7454400371385366819 ) ) ;
#51644=AXIS2_PLACEMENT_3D ( 'NONE', #24787, #18039, #70825 ) ;
#51711=CARTESIAN_POINT ( 'NONE',  ( 11.99999999999999822, -5.801387104618779489, -0.7465129729868814623 ) ) ;
#51874=CARTESIAN_POINT ( 'NONE',  ( -8.000000000000003553, 9.797174393178831574E-16, -25.03750572909317285 ) ) ;
#51915=CARTESIAN_POINT ( 'NONE',  ( -8.000000000000005329, 0.000000000000000000, -14.77459999999999951 ) ) ;
#52043=DIRECTION ( 'NONE',  ( -1.000000000000000000, 0.000000000000000000, -0.000000000000000000 ) ) ;
#52078=ORIENTED_EDGE ( 'NONE', *, *, #51458, .T. ) ;
#52126=CARTESIAN_POINT ( 'NONE',  ( 0.000000000000000000, 0.000000000000000000, 0.000000000000000000 ) ) ;
#52312=DIRECTION ( 'NONE',  ( -1.000000000000000000, 0.000000000000000000, 0.000000000000000000 ) ) ;
#52340=VERTEX_POINT ( 'NONE', #24654 ) ;
#52341=B_SPLINE_CURVE_WITH_KNOTS ( 'NONE', 3,
 ( #21559, #27591, #26462, #15150, #44585, #32911 ),
 .UNSPECIFIED., .F., .F.,
 ( 4, 2, 4 ),
 ( 2.380729645499322951E-07, 0.003505341553885846402, 0.007010445034807142976 ),
 .UNSPECIFIED. ) ;
#52352=DIRECTION ( 'NONE',  ( 0.000000000000000000, 0.000000000000000000, -1.000000000000000000 ) ) ;
#52538=FACE_BOUND ( 'NONE', #62298, .T. ) ;
#52566=CARTESIAN_POINT ( 'NONE',  ( 5.841566664369303132E-15, 13.85640646055103531, -14.80000000000000071 ) ) ;
#52593=DIRECTION ( 'NONE',  ( 0.000000000000000000, 0.000000000000000000, -1.000000000000000000 ) ) ;
#52607=ADVANCED_FACE ( 'NONE', ( #57070 ), #29134, .T. ) ;
#52722=DIRECTION ( 'NONE',  ( 0.000000000000000000, 0.000000000000000000, 1.000000000000000000 ) ) ;
#52885=ORIENTED_EDGE ( 'NONE', *, *, #15788, .T. ) ;
#53000=CARTESIAN_POINT ( 'NONE',  ( -6.000000000000012434, 10.39230484541325694, 0.000000000000000000 ) ) ;
#53065=VERTEX_POINT ( 'NONE', #60970 ) ;
#53157=FACE_OUTER_BOUND ( 'NONE', #32772, .T. ) ;
#53356=CARTESIAN_POINT ( 'NONE',  ( 0.000000000000000000, 0.000000000000000000, -0.7002075382097148193 ) ) ;
#53469=CARTESIAN_POINT ( 'NONE',  ( 7.806255641895631925E-15, 13.85640646055103709, -1.071796769724504550 ) ) ;
#53503=DIRECTION ( 'NONE',  ( -1.000000000000000000, 0.000000000000000000, -0.000000000000000000 ) ) ;
#53589=ADVANCED_FACE ( 'NONE', ( #39180 ), #56544, .T. ) ;
#53727=CIRCLE ( 'NONE', #70587, 12.00000000000000178 ) ;
#53767=ADVANCED_FACE ( 'NONE', ( #68970 ), #11999, .T. ) ;
#53915=( LENGTH_UNIT ( ) NAMED_UNIT ( * ) SI_UNIT ( .MILLI., .METRE. ) );
#53932=DIRECTION ( 'NONE',  ( -1.000000000000000000, 0.000000000000000000, 0.000000000000000000 ) ) ;
#54042=CARTESIAN_POINT ( 'NONE',  ( 8.000000000000003553, 0.000000000000000000, -25.03750572909317285 ) ) ;
#54080=FACE_OUTER_BOUND ( 'NONE', #4053, .T. ) ;
#54133=LINE ( 'NONE', #65807, #29037 ) ;
#54158=ADVANCED_FACE ( 'NONE', ( #57200 ), #28515, .F. ) ;
#54420=VERTEX_POINT ( 'NONE', #60144 ) ;
#54474=CIRCLE ( 'NONE', #23117, 12.00000000000000000 ) ;
#54487=DIRECTION ( 'NONE',  ( -0.000000000000000000, -0.000000000000000000, 1.000000000000000000 ) ) ;
#54652=EDGE_LOOP ( 'NONE', ( #65312, #22179, #38529 ) ) ;
#54744=VECTOR ( 'NONE', #30296, 1000.000000000000000 ) ;
#54775=CARTESIAN_POINT ( 'NONE',  ( 0.000000000000000000, 0.000000000000000000, 0.000000000000000000 ) ) ;
#54897=ORIENTED_EDGE ( 'NONE', *, *, #34553, .T. ) ;
#54899=B_SPLINE_CURVE_WITH_KNOTS ( 'NONE', 3,
 ( #729, #5257, #57692, #11282, #28629, #63697, #51641, #56941 ),
 .UNSPECIFIED., .F., .F.,
 ( 4, 2, 2, 4 ),
 ( 0.007010445034807182875, 0.008756443665256715206, 0.01050244229570624840, 0.01399443955660531827 ),
 .UNSPECIFIED. ) ;
#54930=AXIS2_PLACEMENT_3D ( 'NONE', #48402, #64657, #48030 ) ;
#55066=FACE_BOUND ( 'NONE', #65698, .T. ) ;
#55076=ORIENTED_EDGE ( 'NONE', *, *, #2954, .F. ) ;
#55152=ADVANCED_FACE ( 'NONE', ( #63425 ), #9573, .T. ) ;
#55298=CARTESIAN_POINT ( 'NONE',  ( -6.000000000000021316, -10.39230484541325161, 0.000000000000000000 ) ) ;
#55478=AXIS2_PLACEMENT_3D ( 'NONE', #27234, #38580, #32549 ) ;
#55580=VERTEX_POINT ( 'NONE', #51030 ) ;
#55749=CARTESIAN_POINT ( 'NONE',  ( 0.000000000000000000, 0.000000000000000000, -14.77459999999999951 ) ) ;
#55775=AXIS2_PLACEMENT_3D ( 'NONE', #17996, #51577, #58017 ) ;
#55817=FACE_OUTER_BOUND ( 'NONE', #19893, .T. ) ;
#55876=ORIENTED_EDGE ( 'NONE', *, *, #3880, .F. ) ;
#55897=ORIENTED_EDGE ( 'NONE', *, *, #35227, .T. ) ;
#55903=VECTOR ( 'NONE', #40547, 1000.000000000000000 ) ;
#56157=AXIS2_PLACEMENT_3D ( 'NONE', #25011, #72157, #3141 ) ;
#56263=EDGE_LOOP ( 'NONE', ( #51191, #12307, #73590, #20293 ) ) ;
#56426=B_SPLINE_CURVE_WITH_KNOTS ( 'NONE', 3,
 ( #5698, #51711, #58, #17375, #46050, #29819 ),
 .UNSPECIFIED., .F., .F.,
 ( 4, 2, 4 ),
 ( 0.01236082503524029742, 0.01586526280559109534, 0.01936970057594189498 ),
 .UNSPECIFIED. ) ;
#56544=CYLINDRICAL_SURFACE ( 'NONE', #57732, 12.00000000000000355 ) ;
#56610=VERTEX_POINT ( 'NONE', #9589 ) ;
#56617=EDGE_CURVE ( 'NONE', #18980, #34052, #68688, .T. ) ;
#56656=CARTESIAN_POINT ( 'NONE',  ( -6.000000000000037303, -10.39230484541327826, -14.00000000000000178 ) ) ;
#56877=CARTESIAN_POINT ( 'NONE',  ( 0.000000000000000000, 0.000000000000000000, -14.00000000000000178 ) ) ;
#56941=CARTESIAN_POINT ( 'NONE',  ( 12.00000000000000000, 6.928203230275542523, -1.071796769724504550 ) ) ;
#57028=DIRECTION ( 'NONE',  ( 0.000000000000000000, -1.000000000000000000, 0.000000000000000000 ) ) ;
#57046=AXIS2_PLACEMENT_3D ( 'NONE', #42270, #69848, #65281 ) ;
#57070=FACE_OUTER_BOUND ( 'NONE', #1582, .T. ) ;
#57173=EDGE_CURVE ( 'NONE', #52340, #64048, #7247, .T. ) ;
#57200=FACE_OUTER_BOUND ( 'NONE', #20358, .T. ) ;
#57208=FACE_OUTER_BOUND ( 'NONE', #122, .T. ) ;
#57304=CIRCLE ( 'NONE', #64566, 8.000000000000005329 ) ;
#57354=AXIS2_PLACEMENT_3D ( 'NONE', #63097, #11422, #34459 ) ;
#57370=VECTOR ( 'NONE', #66487, 1000.000000000000000 ) ;
#57403=CARTESIAN_POINT ( 'NONE',  ( 0.000000000000000000, 0.000000000000000000, 0.000000000000000000 ) ) ;
#57433=ORIENTED_EDGE ( 'NONE', *, *, #38714, .T. ) ;
#57505=LINE ( 'NONE', #52566, #54744 ) ;
#57601=DIRECTION ( 'NONE',  ( 0.000000000000000000, 0.000000000000000000, 1.000000000000000000 ) ) ;
#57691=VERTEX_POINT ( 'NONE', #72011 ) ;
#57692=CARTESIAN_POINT ( 'NONE',  ( 7.020684431968935435, 9.803012413858334995, -0.02533325329315222127 ) ) ;
#57695=AXIS2_PLACEMENT_3D ( 'NONE', #60704, #14662, #53932 ) ;
#57732=AXIS2_PLACEMENT_3D ( 'NONE', #4861, #27857, #15035 ) ;
#57819=ORIENTED_EDGE ( 'NONE', *, *, #70879, .T. ) ;
#57822=DIRECTION ( 'NONE',  ( -0.5000000000000017764, -0.8660254037844377084, 0.000000000000000000 ) ) ;
#58017=DIRECTION ( 'NONE',  ( -1.000000000000000000, 0.000000000000000000, 0.000000000000000000 ) ) ;
#58031=FACE_OUTER_BOUND ( 'NONE', #42532, .T. ) ;
#58040=VERTEX_POINT ( 'NONE', #34366 ) ;
#58147=FACE_OUTER_BOUND ( 'NONE', #54652, .T. ) ;
#58364=EDGE_CURVE ( 'NONE', #62698, #53065, #43415, .T. ) ;
#58468=ADVANCED_FACE ( 'NONE', ( #52538, #139 ), #876, .T. ) ;
#58734=CARTESIAN_POINT ( 'NONE',  ( -3.255014963930524218E-15, -13.85640646055106728, -14.80000000000000071 ) ) ;
#58749=AXIS2_PLACEMENT_3D ( 'NONE', #61262, #48440, #26925 ) ;
#58915=ORIENTED_EDGE ( 'NONE', *, *, #28909, .T. ) ;
#59026=AXIS2_PLACEMENT_3D ( 'NONE', #6454, #29457, #24148 ) ;
#59199=VECTOR ( 'NONE', #25283, 1000.000000000000000 ) ;
#59231=AXIS2_PLACEMENT_3D ( 'NONE', #45495, #45873, #39843 ) ;
#59247=CARTESIAN_POINT ( 'NONE',  ( -6.331740687315345895E-14, -13.85640646055103531, -1.071796769724504550 ) ) ;
#59456=ORIENTED_EDGE ( 'NONE', *, *, #71167, .T. ) ;
#59466=ORIENTED_EDGE ( 'NONE', *, *, #3880, .T. ) ;
#59612=ORIENTED_EDGE ( 'NONE', *, *, #1319, .T. ) ;
#59657=CARTESIAN_POINT ( 'NONE',  ( -7.020684431968946093, -9.803012413858361640, -0.02533325329316988769 ) ) ;
#59673=ORIENTED_EDGE ( 'NONE', *, *, #41593, .F. ) ;
#59781=EDGE_CURVE ( 'NONE', #19, #5379, #56426, .T. ) ;
#60025=CARTESIAN_POINT ( 'NONE',  ( 5.841566664369303132E-15, 13.85640646055103531, -14.00000000000000178 ) ) ;
#60032=LINE ( 'NONE', #25320, #26129 ) ;
#60040=ORIENTED_EDGE ( 'NONE', *, *, #16611, .F. ) ;
#60144=CARTESIAN_POINT ( 'NONE',  ( 6.000000000000024869, 10.39230484541325339, -14.00000000000000178 ) ) ;
#60368=AXIS2_PLACEMENT_3D ( 'NONE', #57403, #73623, #62297 ) ;
#60389=CARTESIAN_POINT ( 'NONE',  ( -6.000000000000021316, -10.39230484541325161, 0.000000000000000000 ) ) ;
#60528=DIRECTION ( 'NONE',  ( -1.000000000000000000, 0.000000000000000000, 0.000000000000000000 ) ) ;
#60590=CIRCLE ( 'NONE', #55775, 12.00000000000000000 ) ;
#60621=ADVANCED_FACE ( 'NONE', ( #32626 ), #17914, .T. ) ;
#60637=DIRECTION ( 'NONE',  ( 0.000000000000000000, 0.000000000000000000, -1.000000000000000000 ) ) ;
#60704=CARTESIAN_POINT ( 'NONE',  ( 0.000000000000000000, 0.000000000000000000, -14.80000000000000071 ) ) ;
#60825=FACE_OUTER_BOUND ( 'NONE', #72824, .T. ) ;
#60826=CARTESIAN_POINT ( 'NONE',  ( -11.99999999999999822, 4.673005023400501834, -0.4790896970872564609 ) ) ;
#60970=CARTESIAN_POINT ( 'NONE',  ( 12.00000000000000000, 0.000000000000000000, -14.00000000000000178 ) ) ;
#61004=LINE ( 'NONE', #69648, #11069 ) ;
#61195=DIRECTION ( 'NONE',  ( 0.000000000000000000, 0.000000000000000000, 1.000000000000000000 ) ) ;
#61262=CARTESIAN_POINT ( 'NONE',  ( 0.000000000000000000, 0.000000000000000000, -0.7702282920306856573 ) ) ;
#61333=CONICAL_SURFACE ( 'NONE', #44474, 12.00000000000000000, 1.047197551196596077 ) ;
#61337=ADVANCED_FACE ( 'NONE', ( #46355 ), #69372, .T. ) ;
#61515=AXIS2_PLACEMENT_3D ( 'NONE', #32672, #66604, #26986 ) ;
#61691=ORIENTED_EDGE ( 'NONE', *, *, #48064, .F. ) ;
#62010=LINE ( 'NONE', #21268, #71699 ) ;
#62207=CARTESIAN_POINT ( 'NONE',  ( -12.00000000000000000, -5.801387104618788371, -0.7465129729868831276 ) ) ;
#62267=ORIENTED_EDGE ( 'NONE', *, *, #67372, .T. ) ;
#62296=DIRECTION ( 'NONE',  ( -0.8660254037844374864, 0.5000000000000018874, 0.000000000000000000 ) ) ;
#62297=DIRECTION ( 'NONE',  ( -1.000000000000000000, -1.776356839400250465E-15, 0.000000000000000000 ) ) ;
#62298=EDGE_LOOP ( 'NONE', ( #39266, #54897 ) ) ;
#62350=VERTEX_POINT ( 'NONE', #43566 ) ;
#62622=ADVANCED_FACE ( 'NONE', ( #19258 ), #29485, .T. ) ;
#62636=ORIENTED_EDGE ( 'NONE', *, *, #24704, .T. ) ;
#62682=VERTEX_POINT ( 'NONE', #1569 ) ;
#62698=VERTEX_POINT ( 'NONE', #14707 ) ;
#62954=CARTESIAN_POINT ( 'NONE',  ( -12.00000000000000178, -1.170752406943654123, -5.082197683525801418E-17 ) ) ;
#63097=CARTESIAN_POINT ( 'NONE',  ( 0.000000000000000000, 0.000000000000000000, 0.000000000000000000 ) ) ;
#63103=EDGE_LOOP ( 'NONE', ( #8898, #36340, #9133, #15791 ) ) ;
#63126=( NAMED_UNIT ( * ) SI_UNIT ( $, .STERADIAN. ) SOLID_ANGLE_UNIT ( ) );
#63358=ORIENTED_EDGE ( 'NONE', *, *, #6304, .T. ) ;
#63425=FACE_OUTER_BOUND ( 'NONE', #75, .T. ) ;
#63479=DIRECTION ( 'NONE',  ( 0.000000000000000000, 0.000000000000000000, -1.000000000000000000 ) ) ;
#63489=DIRECTION ( 'NONE',  ( -0.5000000000000011102, 0.8660254037844380415, 0.000000000000000000 ) ) ;
#63549=STYLED_ITEM('',(#74706),#40373);
#63592=LINE ( 'NONE', #51915, #19458 ) ;
#63605=B_SPLINE_CURVE_WITH_KNOTS ( 'NONE', 3,
 ( #39204, #62207, #21470, #74272, #62954, #68246 ),
 .UNSPECIFIED., .F., .F.,
 ( 4, 2, 4 ),
 ( 0.01236082503524027314, 0.01586526280559107799, 0.01936970057594187763 ),
 .UNSPECIFIED. ) ;
#63697=CARTESIAN_POINT ( 'NONE',  ( 10.03369110562687361, 8.063452199751775851, -0.4760262082327572641 ) ) ;
#63833=EDGE_CURVE ( 'NONE', #68525, #22045, #68844, .T. ) ;
#64015=DIRECTION ( 'NONE',  ( 0.8660254037844380415, 0.5000000000000009992, 0.000000000000000000 ) ) ;
#64019=AXIS2_PLACEMENT_3D ( 'NONE', #5281, #16952, #52043 ) ;
#64048=VERTEX_POINT ( 'NONE', #30335 ) ;
#64167=EDGE_CURVE ( 'NONE', #34052, #18980, #51040, .T. ) ;
#64282=DIRECTION ( 'NONE',  ( -1.000000000000000000, 0.000000000000000000, 0.000000000000000000 ) ) ;
#64412=PLANE ( 'NONE',  #26995 ) ;
#64478=DIRECTION ( 'NONE',  ( 0.000000000000000000, 0.000000000000000000, -1.000000000000000000 ) ) ;
#64507=VERTEX_POINT ( 'NONE', #27642 ) ;
#64545=APPLICATION_CONTEXT ( 'automotive_design' ) ;
#64565=EDGE_LOOP ( 'NONE', ( #55897, #3675, #27219, #19757 ) ) ;
#64566=AXIS2_PLACEMENT_3D ( 'NONE', #21340, #14922, #15295 ) ;
#64636=LINE ( 'NONE', #69931, #20385 ) ;
#64657=DIRECTION ( 'NONE',  ( 0.000000000000000000, -0.000000000000000000, 1.000000000000000000 ) ) ;
#64675=AXIS2_PLACEMENT_3D ( 'NONE', #49337, #72353, #2206 ) ;
#64680=ORIENTED_EDGE ( 'NONE', *, *, #10147, .F. ) ;
#65136=CARTESIAN_POINT ( 'NONE',  ( -5.490800045006637653, 10.68629157650003236, 6.075767330655096332E-15 ) ) ;
#65266=CARTESIAN_POINT ( 'NONE',  ( 12.00000000000000178, 2.352228297136963242, -0.1238145317436998294 ) ) ;
#65281=DIRECTION ( 'NONE',  ( -1.000000000000000000, 0.000000000000000000, -0.000000000000000000 ) ) ;
#65312=ORIENTED_EDGE ( 'NONE', *, *, #9063, .F. ) ;
#65492=LINE ( 'NONE', #13784, #6333 ) ;
#65687=ORIENTED_EDGE ( 'NONE', *, *, #58364, .F. ) ;
#65698=EDGE_LOOP ( 'NONE', ( #5167, #55076 ) ) ;
#65777=CARTESIAN_POINT ( 'NONE',  ( 7.000000000000000000, 0.000000000000000000, -14.07439246179028203 ) ) ;
#65807=CARTESIAN_POINT ( 'NONE',  ( -12.00000000000000000, -6.928203230275527424, -14.00000000000000178 ) ) ;
#65880=CARTESIAN_POINT ( 'NONE',  ( -12.00000000000000355, 1.469576158976824342E-15, 0.000000000000000000 ) ) ;
#65896=CARTESIAN_POINT ( 'NONE',  ( 0.000000000000000000, 0.000000000000000000, -25.03750572909317285 ) ) ;
#65917=FACE_OUTER_BOUND ( 'NONE', #20817, .T. ) ;
#65949=ORIENTED_EDGE ( 'NONE', *, *, #18626, .T. ) ;
#65968=ORIENTED_EDGE ( 'NONE', *, *, #1319, .F. ) ;
#66018=CARTESIAN_POINT ( 'NONE',  ( 0.000000000000000000, 0.000000000000000000, 0.000000000000000000 ) ) ;
#66182=DIRECTION ( 'NONE',  ( 0.000000000000000000, 0.000000000000000000, 1.000000000000000000 ) ) ;
#66431=CIRCLE ( 'NONE', #36351, 12.00000000000000355 ) ;
#66487=DIRECTION ( 'NONE',  ( 0.000000000000000000, 0.000000000000000000, 1.000000000000000000 ) ) ;
#66560=CIRCLE ( 'NONE', #34077, 12.00000000000000000 ) ;
#66604=DIRECTION ( 'NONE',  ( -0.000000000000000000, -0.000000000000000000, 1.000000000000000000 ) ) ;
#66779=DIRECTION ( 'NONE',  ( 1.000000000000000000, 0.000000000000000000, 0.000000000000000000 ) ) ;
#66847=CARTESIAN_POINT ( 'NONE',  ( 0.000000000000000000, 0.000000000000000000, -14.00000000000000178 ) ) ;
#66906=ORIENTED_EDGE ( 'NONE', *, *, #30530, .F. ) ;
#66963=CARTESIAN_POINT ( 'NONE',  ( 11.01847871666547540, -7.494884807424072370, -0.7446230086126919279 ) ) ;
#66973=CARTESIAN_POINT ( 'NONE',  ( -1.970211975628493262, -12.71890404606132918, -0.4750804646944283838 ) ) ;
#67097=CARTESIAN_POINT ( 'NONE',  ( 0.000000000000000000, 0.000000000000000000, -14.00000000000000178 ) ) ;
#67252=CARTESIAN_POINT ( 'NONE',  ( -7.000000000000000000, 8.572527594031473190E-16, -14.80000000000000071 ) ) ;
#67372=EDGE_CURVE ( 'NONE', #53065, #72148, #62010, .T. ) ;
#67465=DIRECTION ( 'NONE',  ( 0.8660254037844380415, 0.5000000000000009992, 0.000000000000000000 ) ) ;
#67466=EDGE_CURVE ( 'NONE', #64048, #56610, #29011, .T. ) ;
#67616=CARTESIAN_POINT ( 'NONE',  ( -12.00000000000000000, 6.928203230275504332, -1.071796769724504550 ) ) ;
#67736=CONICAL_SURFACE ( 'NONE', #35211, 8.000000000000005329, 0.9599310885968794782 ) ;
#67828=EDGE_CURVE ( 'NONE', #37361, #22045, #57304, .T. ) ;
#67841=CARTESIAN_POINT ( 'NONE',  ( 0.000000000000000000, 0.000000000000000000, -25.03750572909317285 ) ) ;
#67874=ORIENTED_EDGE ( 'NONE', *, *, #73203, .F. ) ;
#67876=AXIS2_PLACEMENT_3D ( 'NONE', #28383, #57822, #51392 ) ;
#67964=LINE ( 'NONE', #16257, #71634 ) ;
#68057=VECTOR ( 'NONE', #57028, 1000.000000000000000 ) ;
#68246=CARTESIAN_POINT ( 'NONE',  ( -12.00000000000000000, 0.000000000000000000, 0.000000000000000000 ) ) ;
#68303=VERTEX_POINT ( 'NONE', #65777 ) ;
#68513=CYLINDRICAL_SURFACE ( 'NONE', #59231, 7.000000000000000000 ) ;
#68525=VERTEX_POINT ( 'NONE', #50292 ) ;
#68688=CIRCLE ( 'NONE', #15640, 7.000000000000000000 ) ;
#68765=ORIENTED_EDGE ( 'NONE', *, *, #67466, .T. ) ;
#68775=CARTESIAN_POINT ( 'NONE',  ( 0.000000000000000000, 0.000000000000000000, -0.7002075382097148193 ) ) ;
#68844=LINE ( 'NONE', #51874, #55903 ) ;
#68970=FACE_OUTER_BOUND ( 'NONE', #761, .T. ) ;
#69007=AXIS2_PLACEMENT_3D ( 'NONE', #37262, #60637, #53503 ) ;
#69137=SHAPE_REPRESENTATION ( 'hexagon nut style 1_is_IS 1364-3 - M16-W-N', ( #57354 ), #27271 ) ;
#69325=CARTESIAN_POINT ( 'NONE',  ( 0.000000000000000000, 23.85640646055104241, -14.00000000000000178 ) ) ;
#69372=PLANE ( 'NONE',  #72132 ) ;
#69526=DIRECTION ( 'NONE',  ( 0.000000000000000000, 0.000000000000000000, -1.000000000000000000 ) ) ;
#69529=CARTESIAN_POINT ( 'NONE',  ( 12.00000000000000000, 6.928203230275491009, -14.00000000000000178 ) ) ;
#69629=DIRECTION ( 'NONE',  ( 0.000000000000000000, 0.000000000000000000, 1.000000000000000000 ) ) ;
#69648=CARTESIAN_POINT ( 'NONE',  ( -3.255014963930524218E-15, -13.85640646055106728, -14.00000000000000178 ) ) ;
#69659=CARTESIAN_POINT ( 'NONE',  ( 0.000000000000000000, 0.000000000000000000, -14.77459999999999951 ) ) ;
#69793=ORIENTED_EDGE ( 'NONE', *, *, #5361, .F. ) ;
#69833=CARTESIAN_POINT ( 'NONE',  ( 12.00000000000000000, 6.928203230275542523, -1.071796769724504550 ) ) ;
#69848=DIRECTION ( 'NONE',  ( 0.000000000000000000, 0.000000000000000000, -1.000000000000000000 ) ) ;
#69931=CARTESIAN_POINT ( 'NONE',  ( -12.00000000000000000, 6.928203230275504332, -14.00000000000000178 ) ) ;
#70439=CARTESIAN_POINT ( 'NONE',  ( -3.255014963930524218E-15, -13.85640646055106728, -14.80000000000000071 ) ) ;
#70446=CARTESIAN_POINT ( 'NONE',  ( -0.9790701977573761372, 13.29114001832026837, -0.7454400371385527801 ) ) ;
#70478=CARTESIAN_POINT ( 'NONE',  ( 7.806255641895631925E-15, 13.85640646055103709, -1.071796769724504550 ) ) ;
#70568=CARTESIAN_POINT ( 'NONE',  ( 12.00000000000000178, 5.807951393103206073, -0.7484079198486913720 ) ) ;
#70587=AXIS2_PLACEMENT_3D ( 'NONE', #49145, #14435, #13321 ) ;
#70731=AXIS2_PLACEMENT_3D ( 'NONE', #20824, #61195, #71749 ) ;
#70798=EDGE_CURVE ( 'NONE', #54420, #48595, #48762, .T. ) ;
#70808=ORIENTED_EDGE ( 'NONE', *, *, #7521, .F. ) ;
#70810=EDGE_CURVE ( 'NONE', #21543, #12103, #52341, .T. ) ;
#70825=DIRECTION ( 'NONE',  ( -1.000000000000000000, 0.000000000000000000, 0.000000000000000000 ) ) ;
#70843=PLANE ( 'NONE',  #69007 ) ;
#70879=EDGE_CURVE ( 'NONE', #54420, #58040, #67964, .T. ) ;
#70940=VERTEX_POINT ( 'NONE', #56656 ) ;
#71073=VECTOR ( 'NONE', #20221, 1000.000000000000000 ) ;
#71167=EDGE_CURVE ( 'NONE', #55580, #53065, #17012, .T. ) ;
#71233=ORIENTED_EDGE ( 'NONE', *, *, #67466, .F. ) ;
#71294=EDGE_CURVE ( 'NONE', #55580, #73846, #18874, .T. ) ;
#71455=CARTESIAN_POINT ( 'NONE',  ( -12.00000000000000000, -6.928203230275527424, -14.80000000000000071 ) ) ;
#71556=CARTESIAN_POINT ( 'NONE',  ( 0.000000000000000000, 0.000000000000000000, 3.469446951953614189E-15 ) ) ;
#71634=VECTOR ( 'NONE', #62296, 1000.000000000000114 ) ;
#71655=CARTESIAN_POINT ( 'NONE',  ( 0.000000000000000000, 0.000000000000000000, 0.000000000000000000 ) ) ;
#71699=VECTOR ( 'NONE', #27676, 1000.000000000000000 ) ;
#71746=AXIS2_PLACEMENT_3D ( 'NONE', #58734, #17237, #64015 ) ;
#71749=DIRECTION ( 'NONE',  ( 1.000000000000000000, 0.000000000000000000, 0.000000000000000000 ) ) ;
#71795=CIRCLE ( 'NONE', #54930, 12.00000000000000355 ) ;
#71904=PRODUCT_DEFINITION_FORMATION_WITH_SPECIFIED_SOURCE ( 'ANY', '', #42631, .NOT_KNOWN. ) ;
#71910=ORIENTED_EDGE ( 'NONE', *, *, #11098, .F. ) ;
#72011=CARTESIAN_POINT ( 'NONE',  ( -6.331740687315345895E-14, -13.85640646055103531, -1.071796769724504550 ) ) ;
#72132=AXIS2_PLACEMENT_3D ( 'NONE', #17682, #12028, #35061 ) ;
#72137=CARTESIAN_POINT ( 'NONE',  ( -12.00000000000000178, 1.173324140324972342, -0.02489140746004457963 ) ) ;
#72148=VERTEX_POINT ( 'NONE', #7393 ) ;
#72157=DIRECTION ( 'NONE',  ( -0.000000000000000000, -0.000000000000000000, 1.000000000000000000 ) ) ;
#72213=DIRECTION ( 'NONE',  ( 0.000000000000000000, 0.000000000000000000, -1.000000000000000000 ) ) ;
#72247=ADVANCED_BREP_SHAPE_REPRESENTATION ( '', ( #40373, #57354 ), #27271 ) ;
#72257=CONICAL_SURFACE ( 'NONE', #59026, 12.00000000000000000, 1.047197551196596077 ) ;
#72263=VERTEX_POINT ( 'NONE', #22404 ) ;
#72353=DIRECTION ( 'NONE',  ( 0.000000000000000000, 0.000000000000000000, -1.000000000000000000 ) ) ;
#72761=CYLINDRICAL_SURFACE ( 'NONE', #47028, 8.000000000000003553 ) ;
#72796=CARTESIAN_POINT ( 'NONE',  ( 3.968262987731704605, 11.56532875636889557, -0.1021479564361147535 ) ) ;
#72824=EDGE_LOOP ( 'NONE', ( #41052, #73936, #34618, #28595 ) ) ;
#72999=CARTESIAN_POINT ( 'NONE',  ( 6.000000000000011546, -10.39230484541325694, 0.000000000000000000 ) ) ;
#73203=EDGE_CURVE ( 'NONE', #70940, #62698, #30792, .T. ) ;
#73420=CARTESIAN_POINT ( 'NONE',  ( 12.00000000000000355, -6.928203230275539859, -1.071796769724504550 ) ) ;
#73543=ADVANCED_FACE ( 'NONE', ( #35719 ), #30053, .T. ) ;
#73555=CARTESIAN_POINT ( 'NONE',  ( 0.000000000000000000, 0.000000000000000000, 0.000000000000000000 ) ) ;
#73590=ORIENTED_EDGE ( 'NONE', *, *, #47311, .T. ) ;
#73604=DIRECTION ( 'NONE',  ( 0.000000000000000000, -0.000000000000000000, 1.000000000000000000 ) ) ;
#73623=DIRECTION ( 'NONE',  ( 0.000000000000000000, -0.000000000000000000, 1.000000000000000000 ) ) ;
#73846=VERTEX_POINT ( 'NONE', #1762 ) ;
#73936=ORIENTED_EDGE ( 'NONE', *, *, #64167, .T. ) ;
#74034=EDGE_CURVE ( 'NONE', #57691, #64048, #17465, .T. ) ;
#74149=DIRECTION ( 'NONE',  ( 0.8191520442889885789, 0.000000000000000000, 0.5735764363510507113 ) ) ;
#74170=DIRECTION ( 'NONE',  ( -0.000000000000000000, -0.000000000000000000, 1.000000000000000000 ) ) ;
#74225=ORIENTED_EDGE ( 'NONE', *, *, #1410, .F. ) ;
#74232=ORIENTED_EDGE ( 'NONE', *, *, #14936, .F. ) ;
#74235=LINE ( 'NONE', #27093, #24568 ) ;
#74272=CARTESIAN_POINT ( 'NONE',  ( -12.00000000000000178, -2.333919766284222597, -0.1006330532450335213 ) ) ;
#74388=EDGE_CURVE ( 'NONE', #20958, #15222, #71795, .T. ) ;
#74407=ADVANCED_FACE ( 'NONE', ( #54080 ), #18998, .T. ) ;
#74467=EDGE_CURVE ( 'NONE', #42139, #6656, #11571, .T. ) ;
#74503=EDGE_CURVE ( 'NONE', #48595, #39861, #53727, .T. ) ;
#74548=CYLINDRICAL_SURFACE ( 'NONE', #39789, 12.00000000000000355 ) ;
#74563=LINE ( 'NONE', #51175, #1358 ) ;
#74700=COLOUR_RGB('Black',0.12,0.14,0.17);
#74701=FILL_AREA_STYLE_COLOUR('',#74700);
#74702=FILL_AREA_STYLE('',(#74701));
#74703=SURFACE_STYLE_FILL_AREA(#74702);
#74704=SURFACE_SIDE_STYLE('',(#74703));
#74705=SURFACE_STYLE_USAGE(.BOTH.,#74704);
#74706=PRESENTATION_STYLE_ASSIGNMENT((#74705));
ENDSEC;
END-ISO-10303-21;
